ISO-10303-21;
HEADER;
FILE_DESCRIPTION (('STEP AP214'),
    '1' );
FILE_NAME ('torque nut 08_iso_ISO 10511-M10-N.step',
    '2026-10-23T05:12:30',
    ( '' ),
    ( '' ),
    'SwSTEP 2.0',
    'SolidWorks 2026',
    '' );
FILE_SCHEMA (( 'AUTOMOTIVE_DESIGN' ));
ENDSEC;

DATA;
#9=AXIS2_PLACEMENT_3D ( 'NONE', #5192, #2676, #2095 ) ;
#16=AXIS2_PLACEMENT_3D ( 'NONE', #1817, #35, #4883 ) ;
#35=DIRECTION ( 'NONE',  ( -0.000000000000000000, -0.000000000000000000, 1.000000000000000000 ) ) ;
#36=( NAMED_UNIT ( * ) PLANE_ANGLE_UNIT ( ) SI_UNIT ( $, .RADIAN. ) );
#39=DIRECTION ( 'NONE',  ( 1.000000000000000000, 0.000000000000000000, 0.000000000000000000 ) ) ;
#70=ORIENTED_EDGE ( 'NONE', *, *, #5383, .T. ) ;
#81=EDGE_CURVE ( 'NONE', #1868, #4093, #1608, .T. ) ;
#87=EDGE_LOOP ( 'NONE', ( #2176, #4248, #1916, #2842 ) ) ;
#91=DIRECTION ( 'NONE',  ( 0.000000000000000000, 0.000000000000000000, -1.000000000000000000 ) ) ;
#94=EDGE_CURVE ( 'NONE', #7689, #4484, #451, .T. ) ;
#95=VECTOR ( 'NONE', #2161, 1000.000000000000000 ) ;
#108=AXIS2_PLACEMENT_3D ( 'NONE', #2705, #5693, #1397 ) ;
#111=DIRECTION ( 'NONE',  ( -1.000000000000000000, 0.000000000000000000, 0.000000000000000000 ) ) ;
#112=( NAMED_UNIT ( * ) SI_UNIT ( $, .STERADIAN. ) SOLID_ANGLE_UNIT ( ) );
#115=VERTEX_POINT ( 'NONE', #5393 ) ;
#122=EDGE_CURVE ( 'NONE', #3301, #4257, #4430, .T. ) ;
#124=CARTESIAN_POINT ( 'NONE',  ( 8.000000000000001776, -3.867591403079175372, -4.202324684675417643 ) ) ;
#125=EDGE_CURVE ( 'NONE', #6200, #406, #1228, .T. ) ;
#142=CARTESIAN_POINT ( 'NONE',  ( 8.000000000000000000, 3.871967595402126872, -4.201061386767543482 ) ) ;
#155=ORIENTED_EDGE ( 'NONE', *, *, #176, .F. ) ;
#159=EDGE_CURVE ( 'NONE', #1610, #2529, #7077, .T. ) ;
#170=ADVANCED_FACE ( 'NONE', ( #5231 ), #1395, .T. ) ;
#171=LINE ( 'NONE', #6767, #1288 ) ;
#174=DIRECTION ( 'NONE',  ( -0.8660254037844382635, -0.5000000000000005551, 0.000000000000000000 ) ) ;
#176=EDGE_CURVE ( 'NONE', #406, #5752, #7525, .T. ) ;
#177=CARTESIAN_POINT ( 'NONE',  ( 8.000000000000000000, 4.618802153517013842, -3.985468820183668104 ) ) ;
#183=CARTESIAN_POINT ( 'NONE',  ( 0.000000000000000000, 0.000000000000000000, -4.700000000000000178 ) ) ;
#186=AXIS2_PLACEMENT_3D ( 'NONE', #4038, #490, #7002 ) ;
#211=CARTESIAN_POINT ( 'NONE',  ( 8.000000000000000000, 4.618802153517004072, -4.700000000000000178 ) ) ;
#225=DIRECTION ( 'NONE',  ( -0.5000000000000006661, -0.8660254037844383745, 0.000000000000000000 ) ) ;
#236=CARTESIAN_POINT ( 'NONE',  ( 4.000000000000005329, -6.928203230275506108, 0.000000000000000000 ) ) ;
#238=CONICAL_SURFACE ( 'NONE', #4018, 8.000000000000000000, 1.047197551196596299 ) ;
#241=CARTESIAN_POINT ( 'NONE',  ( -1.313474075707227406, -8.479269695850861766, -4.383279549040158152 ) ) ;
#276=DIRECTION ( 'NONE',  ( 1.000000000000000000, 0.000000000000000000, 0.000000000000000000 ) ) ;
#295=B_SPLINE_CURVE_WITH_KNOTS ( 'NONE', 3,
 ( #3128, #6526, #3715, #4929, #3487, #4111 ),
 .UNSPECIFIED., .F., .F.,
 ( 4, 2, 4 ),
 ( 0.008240550023493524098, 0.01057684187039405026, 0.01291313371729457642 ),
 .UNSPECIFIED. ) ;
#300=CARTESIAN_POINT ( 'NONE',  ( -8.000000000000000000, 1.572549600175615625, -0.06894455525513183691 ) ) ;
#306=ORIENTED_EDGE ( 'NONE', *, *, #3124, .T. ) ;
#309=( GEOMETRIC_REPRESENTATION_CONTEXT ( 3 ) GLOBAL_UNCERTAINTY_ASSIGNED_CONTEXT ( ( #1741 ) ) GLOBAL_UNIT_ASSIGNED_CONTEXT ( ( #1216, #1786, #4884 ) ) REPRESENTATION_CONTEXT ( 'NONE', 'WORKASPACE' ) );
#326=DIRECTION ( 'NONE',  ( -1.000000000000000000, 1.224646799147352961E-16, 0.000000000000000000 ) ) ;
#338=CARTESIAN_POINT ( 'NONE',  ( -8.000000000000000000, 4.618802153517003184, -0.7145311798163286321 ) ) ;
#340=CARTESIAN_POINT ( 'NONE',  ( 0.000000000000000000, 0.000000000000000000, 0.000000000000000000 ) ) ;
#342=ORIENTED_EDGE ( 'NONE', *, *, #1344, .T. ) ;
#359=CARTESIAN_POINT ( 'NONE',  ( -4.250000000000000000, 5.204748896376250699E-16, 2.573333333332999739 ) ) ;
#362=EDGE_CURVE ( 'NONE', #3787, #4597, #6330, .T. ) ;
#375=CARTESIAN_POINT ( 'NONE',  ( 4.000000000000004441, 6.928203230275507885, -4.700000000000000178 ) ) ;
#381=ORIENTED_EDGE ( 'NONE', *, *, #6740, .T. ) ;
#391=DIRECTION ( 'NONE',  ( -1.000000000000000000, 0.000000000000000000, 0.000000000000000000 ) ) ;
#406=VERTEX_POINT ( 'NONE', #4546 ) ;
#410=CARTESIAN_POINT ( 'NONE',  ( -5.354491962338127742, 6.146186931204406179, -0.06809871960542698832 ) ) ;
#412=CARTESIAN_POINT ( 'NONE',  ( 5.355005115540895311, 6.145890662064654286, -0.08224679563971268315 ) ) ;
#419=EDGE_CURVE ( 'NONE', #4484, #2866, #6124, .T. ) ;
#426=EDGE_CURVE ( 'NONE', #1610, #4116, #5242, .T. ) ;
#438=ORIENTED_EDGE ( 'NONE', *, *, #7182, .T. ) ;
#444=FACE_OUTER_BOUND ( 'NONE', #7719, .T. ) ;
#451=LINE ( 'NONE', #5901, #5864 ) ;
#457=DIRECTION ( 'NONE',  ( -0.000000000000000000, -0.000000000000000000, 1.000000000000000000 ) ) ;
#462=AXIS2_PLACEMENT_3D ( 'NONE', #2816, #5271, #4796 ) ;
#467=PLANE ( 'NONE',  #625 ) ;
#474=B_SPLINE_CURVE_WITH_KNOTS ( 'NONE', 3,
 ( #7048, #496, #2210, #412, #3419, #967, #6382, #2870 ),
 .UNSPECIFIED., .F., .F.,
 ( 4, 2, 2, 4 ),
 ( 0.004673709593152164388, 0.005837709341827651208, 0.007001709090503137160, 0.009329708587854108198 ),
 .UNSPECIFIED. ) ;
#483=EDGE_LOOP ( 'NONE', ( #1370, #2403, #2898 ) ) ;
#485=CARTESIAN_POINT ( 'NONE',  ( -6.689127551062010291, -5.375634714784629509, -0.3173508448886595557 ) ) ;
#490=DIRECTION ( 'NONE',  ( 0.000000000000000000, 0.000000000000000000, -1.000000000000000000 ) ) ;
#493=ORIENTED_EDGE ( 'NONE', *, *, #81, .F. ) ;
#496=CARTESIAN_POINT ( 'NONE',  ( 4.339467034331189410, 6.732211846623394003, 4.972295158619556565E-15 ) ) ;
#504=ORIENTED_EDGE ( 'NONE', *, *, #2684, .F. ) ;
#514=CARTESIAN_POINT ( 'NONE',  ( 0.000000000000000000, 0.000000000000000000, -4.700000000000000178 ) ) ;
#515=AXIS2_PLACEMENT_3D ( 'NONE', #5037, #3898, #818 ) ;
#532=DIRECTION ( 'NONE',  ( -0.000000000000000000, -0.000000000000000000, 1.000000000000000000 ) ) ;
#536=CARTESIAN_POINT ( 'NONE',  ( -6.686525924292792133, 5.377136764700155780, -0.3167204509598384177 ) ) ;
#537=CARTESIAN_POINT ( 'NONE',  ( 8.000000000000000000, -3.098204225878171680, -0.3157906771918751465 ) ) ;
#541=DIRECTION ( 'NONE',  ( 1.000000000000000000, 0.000000000000000000, 0.000000000000000000 ) ) ;
#543=EDGE_LOOP ( 'NONE', ( #5445, #2673, #6980, #2672 ) ) ;
#544=VERTEX_POINT ( 'NONE', #2194 ) ;
#577=EDGE_LOOP ( 'NONE', ( #2999, #4050 ) ) ;
#585=CARTESIAN_POINT ( 'NONE',  ( 4.681481898397002794, -6.534749472788152325, -3.252606517456513302E-16 ) ) ;
#591=CARTESIAN_POINT ( 'NONE',  ( -8.000000000000000000, -4.618802153517013842, -0.7145311798163319628 ) ) ;
#593=B_SPLINE_CURVE_WITH_KNOTS ( 'NONE', 3,
 ( #6364, #1707, #3521, #3990, #4698, #6519, #3366, #987 ),
 .UNSPECIFIED., .F., .F.,
 ( 4, 2, 2, 4 ),
 ( 0.004673709593152171327, 0.005837709341827658147, 0.007001709090503144099, 0.009329708587854113402 ),
 .UNSPECIFIED. ) ;
#595=ORIENTED_EDGE ( 'NONE', *, *, #2057, .F. ) ;
#606=CIRCLE ( 'NONE', #5134, 7.999999999999998224 ) ;
#608=PLANE ( 'NONE',  #1351 ) ;
#625=AXIS2_PLACEMENT_3D ( 'NONE', #5366, #6465, #5319 ) ;
#640=CIRCLE ( 'NONE', #5305, 7.999999999999998224 ) ;
#670=EDGE_LOOP ( 'NONE', ( #4030, #5229, #7475 ) ) ;
#691=CARTESIAN_POINT ( 'NONE',  ( -8.000000000000000000, 9.797174393178825657E-16, 2.573333333333333695 ) ) ;
#695=CARTESIAN_POINT ( 'NONE',  ( -4.250000000000000000, 5.204748896376250699E-16, -4.700000000000000178 ) ) ;
#713=CARTESIAN_POINT ( 'NONE',  ( 8.000000000000000000, 3.115336682267008328, -0.3193931313915058801 ) ) ;
#716=CARTESIAN_POINT ( 'NONE',  ( 8.000000000000001776, -1.555946510856142551, -4.632911297836646014 ) ) ;
#723=CARTESIAN_POINT ( 'NONE',  ( 6.713333333332999864, 0.000000000000000000, 2.573333333332999739 ) ) ;
#724=VECTOR ( 'NONE', #4787, 1000.000000000000000 ) ;
#725=CARTESIAN_POINT ( 'NONE',  ( -8.000000000000000000, 4.618802153517013842, -3.985468820183668104 ) ) ;
#752=ORIENTED_EDGE ( 'NONE', *, *, #2539, .T. ) ;
#762=DIRECTION ( 'NONE',  ( -0.000000000000000000, -0.000000000000000000, -1.000000000000000000 ) ) ;
#765=AXIS2_PLACEMENT_3D ( 'NONE', #3393, #1015, #7018 ) ;
#766=FACE_OUTER_BOUND ( 'NONE', #2228, .T. ) ;
#772=CARTESIAN_POINT ( 'NONE',  ( 0.000000000000000000, 0.000000000000000000, 3.859999999999999876 ) ) ;
#776=LINE ( 'NONE', #1405, #2918 ) ;
#777=CARTESIAN_POINT ( 'NONE',  ( 4.681481898397003683, -6.534749472788152325, -4.700000000000000178 ) ) ;
#786=CARTESIAN_POINT ( 'NONE',  ( 2.309976723937608778, -7.903938623646878270, -0.1306530452038152101 ) ) ;
#787=CIRCLE ( 'NONE', #5332, 5.000000000000000888 ) ;
#790=CARTESIAN_POINT ( 'NONE',  ( -2.309976723937612331, 7.903938623646864059, -0.1306530452038102419 ) ) ;
#796=DIRECTION ( 'NONE',  ( -0.000000000000000000, -0.000000000000000000, 1.000000000000000000 ) ) ;
#802=CARTESIAN_POINT ( 'NONE',  ( -6.713333333332999864, 8.221462178275489009E-16, 2.573333333332999739 ) ) ;
#812=ORIENTED_EDGE ( 'NONE', *, *, #4653, .T. ) ;
#818=DIRECTION ( 'NONE',  ( 1.000000000000000000, 0.000000000000000000, 0.000000000000000000 ) ) ;
#831=CARTESIAN_POINT ( 'NONE',  ( 8.000000000000000000, -4.618802153517011178, -3.985468820183668104 ) ) ;
#843=EDGE_CURVE ( 'NONE', #4257, #3121, #4817, .T. ) ;
#844=CARTESIAN_POINT ( 'NONE',  ( 8.000000000000000000, 1.572549600175620066, -4.631055444744868410 ) ) ;
#850=AXIS2_PLACEMENT_3D ( 'NONE', #1636, #7199, #4826 ) ;
#873=CARTESIAN_POINT ( 'NONE',  ( 0.000000000000000000, 0.000000000000000000, -4.700000000000000178 ) ) ;
#880=CARTESIAN_POINT ( 'NONE',  ( 8.000000000000000000, -4.618802153517012066, -4.700000000000000178 ) ) ;
#888=ORIENTED_EDGE ( 'NONE', *, *, #4171, .F. ) ;
#892=CYLINDRICAL_SURFACE ( 'NONE', #1896, 4.250000000000000000 ) ;
#900=DIRECTION ( 'NONE',  ( 1.000000000000000000, 0.000000000000000000, 0.000000000000000000 ) ) ;
#906=AXIS2_PLACEMENT_3D ( 'NONE', #3438, #5806, #391 ) ;
#919=LINE ( 'NONE', #211, #3515 ) ;
#920=PLANE ( 'NONE',  #7393 ) ;
#922=AXIS2_PLACEMENT_3D ( 'NONE', #6154, #4808, #39 ) ;
#923=ORIENTED_EDGE ( 'NONE', *, *, #5811, .F. ) ;
#926=VERTEX_POINT ( 'NONE', #5882 ) ;
#930=FACE_OUTER_BOUND ( 'NONE', #1696, .T. ) ;
#947=CARTESIAN_POINT ( 'NONE',  ( -2.081668171172168513E-14, -9.237604307034017026, -3.985468820183668104 ) ) ;
#967=CARTESIAN_POINT ( 'NONE',  ( 6.689127551062004962, 5.375634714784620627, -0.3173508448886543931 ) ) ;
#979=CARTESIAN_POINT ( 'NONE',  ( 3.318518101603007864, 7.321656987762870550, 4.845028458294597151E-15 ) ) ;
#980=VERTEX_POINT ( 'NONE', #4100 ) ;
#987=CARTESIAN_POINT ( 'NONE',  ( -8.000000000000000000, -4.618802153517013842, -3.985468820183668104 ) ) ;
#988=EDGE_CURVE ( 'NONE', #1789, #1868, #7640, .T. ) ;
#992=CYLINDRICAL_SURFACE ( 'NONE', #1860, 5.000000000000000888 ) ;
#1001=CIRCLE ( 'NONE', #7678, 4.250000000000000000 ) ;
#1011=ORIENTED_EDGE ( 'NONE', *, *, #3168, .F. ) ;
#1012=ORIENTED_EDGE ( 'NONE', *, *, #122, .T. ) ;
#1015=DIRECTION ( 'NONE',  ( -0.000000000000000000, -0.000000000000000000, 1.000000000000000000 ) ) ;
#1022=CARTESIAN_POINT ( 'NONE',  ( 2.645508037661878920, 7.710219529346608702, -4.631901280394570719 ) ) ;
#1026=VERTEX_POINT ( 'NONE', #947 ) ;
#1045=CARTESIAN_POINT ( 'NONE',  ( -2.644994884459110907, 7.710515798486362371, -4.617753204360286468 ) ) ;
#1071=ORIENTED_EDGE ( 'NONE', *, *, #5323, .F. ) ;
#1077=CARTESIAN_POINT ( 'NONE',  ( 8.000000000000000000, 4.618802153517004072, -4.700000000000000178 ) ) ;
#1079=FACE_OUTER_BOUND ( 'NONE', #670, .T. ) ;
#1080=ORIENTED_EDGE ( 'NONE', *, *, #2057, .T. ) ;
#1085=CARTESIAN_POINT ( 'NONE',  ( 6.689127551062004962, 5.375634714784622403, -4.382649155111347561 ) ) ;
#1087=DIRECTION ( 'NONE',  ( -0.000000000000000000, -0.000000000000000000, 1.000000000000000000 ) ) ;
#1090=CARTESIAN_POINT ( 'NONE',  ( 6.686525924292793022, -5.377136764700165550, -0.3167204509598423590 ) ) ;
#1101=ORIENTED_EDGE ( 'NONE', *, *, #4523, .F. ) ;
#1118=CONICAL_SURFACE ( 'NONE', #5529, 8.000000000000000000, 1.047197551196596299 ) ;
#1128=CARTESIAN_POINT ( 'NONE',  ( 5.354491962338128630, -6.146186931204413284, -0.06809871960543142921 ) ) ;
#1132=ADVANCED_FACE ( 'NONE', ( #766 ), #5138, .T. ) ;
#1141=ORIENTED_EDGE ( 'NONE', *, *, #1629, .T. ) ;
#1151=ORIENTED_EDGE ( 'NONE', *, *, #419, .F. ) ;
#1159=EDGE_LOOP ( 'NONE', ( #4431, #1815 ) ) ;
#1168=CARTESIAN_POINT ( 'NONE',  ( 8.000000000000000000, -4.618802153517011178, -0.7145311798163319628 ) ) ;
#1175=DIRECTION ( 'NONE',  ( 1.000000000000000000, 0.000000000000000000, 0.000000000000000000 ) ) ;
#1176=CARTESIAN_POINT ( 'NONE',  ( -8.000000000000001776, -3.098204225878171680, -0.3157906771918751465 ) ) ;
#1193=AXIS2_PLACEMENT_3D ( 'NONE', #1638, #6488, #5857 ) ;
#1202=CARTESIAN_POINT ( 'NONE',  ( -4.250000000000000000, 5.204748896376250699E-16, -4.149444346342716194 ) ) ;
#1211=EDGE_LOOP ( 'NONE', ( #888, #3113, #3835, #6079 ) ) ;
#1214=ORIENTED_EDGE ( 'NONE', *, *, #988, .T. ) ;
#1216=( LENGTH_UNIT ( ) NAMED_UNIT ( * ) SI_UNIT ( .MILLI., .METRE. ) );
#1225=CARTESIAN_POINT ( 'NONE',  ( 0.000000000000000000, 0.000000000000000000, -4.700000000000000178 ) ) ;
#1228=B_SPLINE_CURVE_WITH_KNOTS ( 'NONE', 3,
 ( #3576, #4601, #2951, #7006, #7749, #6420 ),
 .UNSPECIFIED., .F., .F.,
 ( 4, 2, 4 ),
 ( 2.380731629626129180E-07, 0.002336973833157558137, 0.004673709593152153112 ),
 .UNSPECIFIED. ) ;
#1240=EDGE_CURVE ( 'NONE', #1722, #5462, #5754, .T. ) ;
#1243=B_SPLINE_CURVE_WITH_KNOTS ( 'NONE', 3,
 ( #2727, #2227, #3318, #4575, #979, #2147 ),
 .UNSPECIFIED., .F., .F.,
 ( 4, 2, 4 ),
 ( 2.380731629561858173E-07, 0.002336973833157559872, 0.004673709593152164388 ),
 .UNSPECIFIED. ) ;
#1255=DIRECTION ( 'NONE',  ( -0.000000000000000000, -0.000000000000000000, 1.000000000000000000 ) ) ;
#1265=CONICAL_SURFACE ( 'NONE', #3540, 8.000000000000000000, 1.047197551196596299 ) ;
#1273=FACE_OUTER_BOUND ( 'NONE', #1702, .T. ) ;
#1280=ADVANCED_FACE ( 'NONE', ( #2778 ), #5770, .T. ) ;
#1281=CARTESIAN_POINT ( 'NONE',  ( 0.000000000000000000, 0.000000000000000000, 3.859999999999999876 ) ) ;
#1288=VECTOR ( 'NONE', #6880, 1000.000000000000000 ) ;
#1289=EDGE_LOOP ( 'NONE', ( #5315, #2029, #3494, #4839 ) ) ;
#1301=CARTESIAN_POINT ( 'NONE',  ( 0.000000000000000000, 0.000000000000000000, 0.000000000000000000 ) ) ;
#1326=ADVANCED_FACE ( 'NONE', ( #1711 ), #992, .F. ) ;
#1342=CARTESIAN_POINT ( 'NONE',  ( 8.000000000000000000, 0.000000000000000000, -4.700000000000000178 ) ) ;
#1344=EDGE_CURVE ( 'NONE', #3392, #7619, #6265, .T. ) ;
#1351=AXIS2_PLACEMENT_3D ( 'NONE', #6056, #3682, #6766 ) ;
#1355=CONICAL_SURFACE ( 'NONE', #2879, 8.000000000000000000, 1.047197551196596299 ) ;
#1360=CARTESIAN_POINT ( 'NONE',  ( -2.081668171172168513E-14, -9.237604307034017026, -3.985468820183668104 ) ) ;
#1365=EDGE_LOOP ( 'NONE', ( #3798, #3024, #2338 ) ) ;
#1367=CARTESIAN_POINT ( 'NONE',  ( 6.686525924292793022, -5.377136764700165550, -4.383279549040157264 ) ) ;
#1370=ORIENTED_EDGE ( 'NONE', *, *, #2358, .F. ) ;
#1376=AXIS2_PLACEMENT_3D ( 'NONE', #772, #4952, #1400 ) ;
#1384=( GEOMETRIC_REPRESENTATION_CONTEXT ( 3 ) GLOBAL_UNCERTAINTY_ASSIGNED_CONTEXT ( ( #4236 ) ) GLOBAL_UNIT_ASSIGNED_CONTEXT ( ( #6039, #36, #3783 ) ) REPRESENTATION_CONTEXT ( 'NONE', 'WORKASPACE' ) );
#1388=CARTESIAN_POINT ( 'NONE',  ( -4.000000000000004441, 6.928203230275506108, 0.000000000000000000 ) ) ;
#1395=CONICAL_SURFACE ( 'NONE', #2425, 8.000000000000000000, 1.047197551196596299 ) ;
#1397=DIRECTION ( 'NONE',  ( 0.000000000000000000, 0.000000000000000000, 1.000000000000000000 ) ) ;
#1400=DIRECTION ( 'NONE',  ( 1.000000000000000000, 0.000000000000000000, 0.000000000000000000 ) ) ;
#1402=ORIENTED_EDGE ( 'NONE', *, *, #1747, .F. ) ;
#1405=CARTESIAN_POINT ( 'NONE',  ( -5.857142857142855874, 7.172931252148781134E-16, 9.480888224575629408 ) ) ;
#1424=DIRECTION ( 'NONE',  ( -1.000000000000000000, 0.000000000000000000, 0.000000000000000000 ) ) ;
#1433=SHAPE_REPRESENTATION ( 'torque nut 08_iso_ISO 10511-M10-N', ( #7485 ), #309 ) ;
#1442=ORIENTED_EDGE ( 'NONE', *, *, #5782, .F. ) ;
#1452=CLOSED_SHELL ( 'NONE', ( #6022, #6932, #4288, #1326, #7316, #3316, #3412, #1132, #1867, #4657, #7422, #4128, #2074, #3114, #3945, #5098, #5656, #2984, #6063, #3801, #2170, #3359, #3980, #170, #5923, #3507, #6543, #4032, #6107, #4312, #1724, #2466, #1280 ) ) ;
#1459=CARTESIAN_POINT ( 'NONE',  ( 0.000000000000000000, 0.000000000000000000, -4.700000000000000178 ) ) ;
#1485=ORIENTED_EDGE ( 'NONE', *, *, #5782, .T. ) ;
#1488=DIRECTION ( 'NONE',  ( 0.8660254037844382635, -0.5000000000000005551, 0.000000000000000000 ) ) ;
#1489=FACE_OUTER_BOUND ( 'NONE', #2089, .T. ) ;
#1493=ORIENTED_EDGE ( 'NONE', *, *, #5383, .F. ) ;
#1506=CARTESIAN_POINT ( 'NONE',  ( -0.6543471694412569262, -8.859816792613647962, -4.203584543331202461 ) ) ;
#1520=ORIENTED_EDGE ( 'NONE', *, *, #4655, .T. ) ;
#1527=FACE_OUTER_BOUND ( 'NONE', #6010, .T. ) ;
#1528=DIRECTION ( 'NONE',  ( -1.000000000000000000, 0.000000000000000000, 0.000000000000000000 ) ) ;
#1546=TOROIDAL_SURFACE ( 'NONE', #5699, 6.713333333332999864, 1.286666666666999914 ) ;
#1549=DIRECTION ( 'NONE',  ( 1.000000000000000000, 0.000000000000000000, 0.000000000000000000 ) ) ;
#1550=CONICAL_SURFACE ( 'NONE', #3824, 5.000000000000000888, 0.9599310885968824758 ) ;
#1565=CARTESIAN_POINT ( 'NONE',  ( 8.000000000000000000, -4.618802153517011178, -0.7145311798163319628 ) ) ;
#1566=CARTESIAN_POINT ( 'NONE',  ( -8.000000000000000000, 4.618802153517003184, -0.7145311798163286321 ) ) ;
#1568=DIRECTION ( 'NONE',  ( 0.000000000000000000, 0.000000000000000000, 1.000000000000000000 ) ) ;
#1577=STYLED_ITEM ( 'NONE', ( #3746 ), #7262 ) ;
#1578=CARTESIAN_POINT ( 'NONE',  ( 0.000000000000000000, 0.000000000000000000, 0.000000000000000000 ) ) ;
#1584=DIRECTION ( 'NONE',  ( -0.000000000000000000, -0.000000000000000000, 1.000000000000000000 ) ) ;
#1587=CARTESIAN_POINT ( 'NONE',  ( 4.000000000000005329, -6.928203230275506108, 0.000000000000000000 ) ) ;
#1603=DIRECTION ( 'NONE',  ( -0.000000000000000000, -0.000000000000000000, 1.000000000000000000 ) ) ;
#1604=CYLINDRICAL_SURFACE ( 'NONE', #4640, 5.857142857142855874 ) ;
#1605=DIRECTION ( 'NONE',  ( 1.000000000000000000, 0.000000000000000000, 0.000000000000000000 ) ) ;
#1608=B_SPLINE_CURVE_WITH_KNOTS ( 'NONE', 3,
 ( #375, #1771, #4005, #2991, #5824, #1085, #4162, #4639 ),
 .UNSPECIFIED., .F., .F.,
 ( 4, 2, 2, 4 ),
 ( 0.004673709593152164388, 0.005837709341827650340, 0.007001709090503136293, 0.009329708587854108198 ),
 .UNSPECIFIED. ) ;
#1610=VERTEX_POINT ( 'NONE', #6099 ) ;
#1629=EDGE_CURVE ( 'NONE', #6375, #3955, #7547, .T. ) ;
#1636=CARTESIAN_POINT ( 'NONE',  ( 0.000000000000000000, 0.000000000000000000, -4.700000000000000178 ) ) ;
#1638=CARTESIAN_POINT ( 'NONE',  ( 0.000000000000000000, 0.000000000000000000, 9.480888224575629408 ) ) ;
#1643=DIRECTION ( 'NONE',  ( 0.000000000000000000, 0.000000000000000000, -1.000000000000000000 ) ) ;
#1644=CARTESIAN_POINT ( 'NONE',  ( 0.000000000000000000, 0.000000000000000000, 9.480888224575629408 ) ) ;
#1664=CARTESIAN_POINT ( 'NONE',  ( 0.000000000000000000, 0.000000000000000000, 0.000000000000000000 ) ) ;
#1669=ORIENTED_EDGE ( 'NONE', *, *, #4327, .F. ) ;
#1670=CARTESIAN_POINT ( 'NONE',  ( -7.347286611336973472, -4.995646404165286825, -0.4969600502617561033 ) ) ;
#1683=DIRECTION ( 'NONE',  ( -1.000000000000000000, 0.000000000000000000, 0.000000000000000000 ) ) ;
#1684=LINE ( 'NONE', #4676, #5524 ) ;
#1694=CONICAL_SURFACE ( 'NONE', #5348, 8.000000000000000000, 1.047197551196596299 ) ;
#1696=EDGE_LOOP ( 'NONE', ( #4031, #1485, #7301, #4838 ) ) ;
#1700=CONICAL_SURFACE ( 'NONE', #186, 8.000000000000000000, 1.047197551196596299 ) ;
#1702=EDGE_LOOP ( 'NONE', ( #6978, #306, #5696, #595, #4493, #5519 ) ) ;
#1707=CARTESIAN_POINT ( 'NONE',  ( -4.339467034331194739, -6.732211846623401996, -4.699999999999999289 ) ) ;
#1711=FACE_OUTER_BOUND ( 'NONE', #87, .T. ) ;
#1714=DIRECTION ( 'NONE',  ( 1.000000000000000000, 0.000000000000000000, 0.000000000000000000 ) ) ;
#1720=FACE_OUTER_BOUND ( 'NONE', #483, .T. ) ;
#1722=VERTEX_POINT ( 'NONE', #5735 ) ;
#1724=ADVANCED_FACE ( 'NONE', ( #3922, #5658 ), #920, .F. ) ;
#1725=EDGE_LOOP ( 'NONE', ( #3720, #6967 ) ) ;
#1729=CARTESIAN_POINT ( 'NONE',  ( -2.309976723937611887, 7.903938623646864059, -4.569346954796190019 ) ) ;
#1732=CARTESIAN_POINT ( 'NONE',  ( 8.000000000000000000, -0.7805016046290997878, -3.218725199566340056E-17 ) ) ;
#1741=UNCERTAINTY_MEASURE_WITH_UNIT (LENGTH_MEASURE( 1.000000000000000082E-05 ), #1216, 'distance_accuracy_value', 'NONE');
#1747=EDGE_CURVE ( 'NONE', #115, #7619, #5623, .T. ) ;
#1750=ORIENTED_EDGE ( 'NONE', *, *, #6829, .T. ) ;
#1751=CIRCLE ( 'NONE', #4509, 5.857142857142856762 ) ;
#1766=CIRCLE ( 'NONE', #7416, 5.000000000000000888 ) ;
#1771=CARTESIAN_POINT ( 'NONE',  ( 4.339467034331189410, 6.732211846623394891, -4.700000000000006395 ) ) ;
#1777=CARTESIAN_POINT ( 'NONE',  ( 4.000000000000005329, -6.928203230275506108, 0.000000000000000000 ) ) ;
#1778=EDGE_CURVE ( 'NONE', #2866, #4859, #6018, .T. ) ;
#1786=( NAMED_UNIT ( * ) PLANE_ANGLE_UNIT ( ) SI_UNIT ( $, .RADIAN. ) );
#1789=VERTEX_POINT ( 'NONE', #3813 ) ;
#1801=CARTESIAN_POINT ( 'NONE',  ( -8.000000000000000000, 0.000000000000000000, -4.700000000000000178 ) ) ;
#1815=ORIENTED_EDGE ( 'NONE', *, *, #4850, .F. ) ;
#1817=CARTESIAN_POINT ( 'NONE',  ( 0.000000000000000000, 0.000000000000000000, 19.04999999999997229 ) ) ;
#1818=CARTESIAN_POINT ( 'NONE',  ( -4.000000000000004441, -6.928203230275506108, -4.700000000000000178 ) ) ;
#1834=AXIS2_PLACEMENT_3D ( 'NONE', #4310, #5536, #5389 ) ;
#1836=EDGE_LOOP ( 'NONE', ( #6987, #7334, #5728, #1982, #4147, #7079 ) ) ;
#1837=PRODUCT ( 'torque nut 08_iso_ISO 10511-M10-N', 'torque nut 08_iso_ISO 10511-M10-N', '', ( #3258 ) ) ;
#1839=DIRECTION ( 'NONE',  ( 1.000000000000000000, 0.000000000000000000, 0.000000000000000000 ) ) ;
#1860=AXIS2_PLACEMENT_3D ( 'NONE', #6408, #7540, #1549 ) ;
#1865=CARTESIAN_POINT ( 'NONE',  ( -1.313474075707227851, -8.479269695850861766, -0.3167204509598428586 ) ) ;
#1867=ADVANCED_FACE ( 'NONE', ( #444 ), #2903, .T. ) ;
#1868=VERTEX_POINT ( 'NONE', #5893 ) ;
#1882=VECTOR ( 'NONE', #6026, 1000.000000000000000 ) ;
#1893=ORIENTED_EDGE ( 'NONE', *, *, #2312, .T. ) ;
#1896=AXIS2_PLACEMENT_3D ( 'NONE', #5747, #6860, #1605 ) ;
#1899=ORIENTED_EDGE ( 'NONE', *, *, #4315, .F. ) ;
#1916=ORIENTED_EDGE ( 'NONE', *, *, #7217, .T. ) ;
#1923=FACE_OUTER_BOUND ( 'NONE', #3523, .T. ) ;
#1960=ORIENTED_EDGE ( 'NONE', *, *, #1778, .F. ) ;
#1971=EDGE_CURVE ( 'NONE', #6313, #3054, #3505, .T. ) ;
#1978=CARTESIAN_POINT ( 'NONE',  ( 8.000000000000000000, 4.618802153517013842, -3.985468820183668104 ) ) ;
#1982=ORIENTED_EDGE ( 'NONE', *, *, #3025, .F. ) ;
#1983=VERTEX_POINT ( 'NONE', #1801 ) ;
#2005=CARTESIAN_POINT ( 'NONE',  ( 3.319543390096038493, -7.321065037175432444, -4.683111142572228935 ) ) ;
#2028=CARTESIAN_POINT ( 'NONE',  ( 3.660532965668821692, -7.124194613927628872, -3.335192229813806599E-16 ) ) ;
#2029=ORIENTED_EDGE ( 'NONE', *, *, #3174, .T. ) ;
#2034=AXIS2_PLACEMENT_3D ( 'NONE', #4694, #3597, #3010 ) ;
#2040=APPLICATION_CONTEXT ( 'automotive_design' ) ;
#2042=DIRECTION ( 'NONE',  ( -0.000000000000000000, -0.000000000000000000, 1.000000000000000000 ) ) ;
#2057=EDGE_CURVE ( 'NONE', #6200, #3301, #2435, .T. ) ;
#2074=ADVANCED_FACE ( 'NONE', ( #1273 ), #608, .T. ) ;
#2077=EDGE_CURVE ( 'NONE', #3551, #4859, #5760, .T. ) ;
#2082=PLANE ( 'NONE',  #108 ) ;
#2089=EDGE_LOOP ( 'NONE', ( #4022, #2498, #2483 ) ) ;
#2092=MECHANICAL_DESIGN_GEOMETRIC_PRESENTATION_REPRESENTATION('',(#1577),#7375);
#2095=DIRECTION ( 'NONE',  ( 1.000000000000000000, -1.776356839400250465E-15, 0.000000000000000000 ) ) ;
#2103=ORIENTED_EDGE ( 'NONE', *, *, #3841, .T. ) ;
#2108=ORIENTED_EDGE ( 'NONE', *, *, #5640, .T. ) ;
#2112=B_SPLINE_CURVE_WITH_KNOTS ( 'NONE', 3,
 ( #6259, #2746, #2005, #5065, #3338, #2633, #3227, #1360 ),
 .UNSPECIFIED., .F., .F.,
 ( 4, 2, 2, 4 ),
 ( 0.004673709593152147908, 0.005837709341827642534, 0.007001709090503137160, 0.009329708587854127280 ),
 .UNSPECIFIED. ) ;
#2118=ORIENTED_EDGE ( 'NONE', *, *, #419, .T. ) ;
#2125=CARTESIAN_POINT ( 'NONE',  ( 8.000000000000000000, 3.115336682267008772, -4.380606868608494686 ) ) ;
#2133=ORIENTED_EDGE ( 'NONE', *, *, #159, .T. ) ;
#2134=CARTESIAN_POINT ( 'NONE',  ( -4.000000000000004441, 6.928203230275506108, 0.000000000000000000 ) ) ;
#2135=CARTESIAN_POINT ( 'NONE',  ( -8.000000000000000000, 3.115336682266999446, -0.3193931313915043257 ) ) ;
#2144=CIRCLE ( 'NONE', #5652, 8.000000000000000000 ) ;
#2147=CARTESIAN_POINT ( 'NONE',  ( 4.000000000000004441, 6.928203230275507885, 0.000000000000000000 ) ) ;
#2151=CARTESIAN_POINT ( 'NONE',  ( -4.000000000000004441, -6.928203230275506108, -4.700000000000000178 ) ) ;
#2161=DIRECTION ( 'NONE',  ( 0.000000000000000000, 0.000000000000000000, 1.000000000000000000 ) ) ;
#2163=AXIS2_PLACEMENT_3D ( 'NONE', #5441, #3003, #5406 ) ;
#2170=ADVANCED_FACE ( 'NONE', ( #5614 ), #1355, .T. ) ;
#2176=ORIENTED_EDGE ( 'NONE', *, *, #4177, .T. ) ;
#2182=DIRECTION ( 'NONE',  ( 1.000000000000000000, 0.000000000000000000, 0.000000000000000000 ) ) ;
#2192=CARTESIAN_POINT ( 'NONE',  ( -4.680456609903976606, -6.535341423375598424, -0.01688885742777120058 ) ) ;
#2194=CARTESIAN_POINT ( 'NONE',  ( 4.250000000000000000, 0.000000000000000000, -4.149444346342716194 ) ) ;
#2199=DIRECTION ( 'NONE',  ( -0.000000000000000000, -0.000000000000000000, 1.000000000000000000 ) ) ;
#2200=AXIS2_PLACEMENT_3D ( 'NONE', #340, #1568, #4721 ) ;
#2210=CARTESIAN_POINT ( 'NONE',  ( 4.680456609903970389, 6.535341423375591319, -0.01688885742776586110 ) ) ;
#2218=ORIENTED_EDGE ( 'NONE', *, *, #3985, .T. ) ;
#2219=EDGE_CURVE ( 'NONE', #1026, #3054, #3617, .T. ) ;
#2221=ORIENTED_EDGE ( 'NONE', *, *, #6312, .F. ) ;
#2227=CARTESIAN_POINT ( 'NONE',  ( 0.6543471694412384965, 8.859816792613651515, -0.4964154566687972170 ) ) ;
#2228=EDGE_LOOP ( 'NONE', ( #1080, #1012, #5527, #1071, #155, #5759 ) ) ;
#2242=AXIS2_PLACEMENT_3D ( 'NONE', #5289, #1584, #2849 ) ;
#2248=CARTESIAN_POINT ( 'NONE',  ( -8.000000000000000000, 4.618802153517003184, -0.7145311798163286321 ) ) ;
#2249=DIRECTION ( 'NONE',  ( -0.000000000000000000, -0.000000000000000000, 1.000000000000000000 ) ) ;
#2258=CARTESIAN_POINT ( 'NONE',  ( -8.000000000000000000, 3.115336682267009660, -4.380606868608495574 ) ) ;
#2259=EDGE_CURVE ( 'NONE', #7537, #3787, #1751, .T. ) ;
#2268=CARTESIAN_POINT ( 'NONE',  ( 1.313474075707211641, 8.479269695850861766, -4.383279549040159928 ) ) ;
#2273=CARTESIAN_POINT ( 'NONE',  ( -5.355005115540899752, -6.145890662064662280, -0.08224679563971788732 ) ) ;
#2286=CARTESIAN_POINT ( 'NONE',  ( -4.681481898397000130, 6.534749472788145219, 4.804370876826391523E-15 ) ) ;
#2295=CIRCLE ( 'NONE', #515, 5.000000000000000888 ) ;
#2312=EDGE_CURVE ( 'NONE', #5752, #1868, #5580, .T. ) ;
#2320=CARTESIAN_POINT ( 'NONE',  ( 8.000000000000000000, 0.7809653281576046657, 3.049318610115479988E-17 ) ) ;
#2329=VERTEX_POINT ( 'NONE', #1587 ) ;
#2336=CARTESIAN_POINT ( 'NONE',  ( 7.345652830558762503, -4.996589667937383794, -0.4964154566687976611 ) ) ;
#2338=ORIENTED_EDGE ( 'NONE', *, *, #1240, .F. ) ;
#2342=DIRECTION ( 'NONE',  ( 1.000000000000000000, 0.000000000000000000, 0.000000000000000000 ) ) ;
#2350=EDGE_LOOP ( 'NONE', ( #70, #4932 ) ) ;
#2358=EDGE_CURVE ( 'NONE', #4116, #4257, #3138, .T. ) ;
#2359=CARTESIAN_POINT ( 'NONE',  ( 8.000000000000000000, 4.618802153517013842, -0.7145311798163319628 ) ) ;
#2391=EDGE_LOOP ( 'NONE', ( #3265, #6337, #7699, #7108, #752, #7670 ) ) ;
#2403=ORIENTED_EDGE ( 'NONE', *, *, #6890, .F. ) ;
#2425=AXIS2_PLACEMENT_3D ( 'NONE', #3536, #1643, #1683 ) ;
#2435=LINE ( 'NONE', #7352, #724 ) ;
#2454=EDGE_LOOP ( 'NONE', ( #1141, #6828, #1750, #4646, #923, #1011 ) ) ;
#2466=ADVANCED_FACE ( 'NONE', ( #5525 ), #5400, .T. ) ;
#2483=ORIENTED_EDGE ( 'NONE', *, *, #6829, .F. ) ;
#2496=LINE ( 'NONE', #7336, #7474 ) ;
#2498=ORIENTED_EDGE ( 'NONE', *, *, #2501, .F. ) ;
#2501=EDGE_CURVE ( 'NONE', #980, #1722, #7372, .T. ) ;
#2503=CARTESIAN_POINT ( 'NONE',  ( 8.000000000000000000, 4.618802153517013842, -0.7145311798163319628 ) ) ;
#2529=VERTEX_POINT ( 'NONE', #2503 ) ;
#2539=EDGE_CURVE ( 'NONE', #1983, #406, #606, .T. ) ;
#2543=CONICAL_SURFACE ( 'NONE', #2163, 8.000000000000000000, 1.047197551196596299 ) ;
#2552=DIRECTION ( 'NONE',  ( 0.000000000000000000, 0.000000000000000000, -1.000000000000000000 ) ) ;
#2562=CARTESIAN_POINT ( 'NONE',  ( 8.000000000000000000, 0.000000000000000000, -4.700000000000000178 ) ) ;
#2570=EDGE_LOOP ( 'NONE', ( #7367, #3818, #1214 ) ) ;
#2571=DIRECTION ( 'NONE',  ( -0.000000000000000000, -0.000000000000000000, -1.000000000000000000 ) ) ;
#2581=CARTESIAN_POINT ( 'NONE',  ( 8.000000000000001776, -3.098204225878173457, -4.384209322808125364 ) ) ;
#2582=VERTEX_POINT ( 'NONE', #3422 ) ;
#2618=AXIS2_PLACEMENT_3D ( 'NONE', #5106, #5774, #6294 ) ;
#2623=CARTESIAN_POINT ( 'NONE',  ( 4.000000000000005329, -6.928203230275506108, -4.700000000000000178 ) ) ;
#2630=CARTESIAN_POINT ( 'NONE',  ( -5.000000000000000888, 6.123233995736767268E-16, 19.04999999999997229 ) ) ;
#2633=CARTESIAN_POINT ( 'NONE',  ( 1.310872448937989931, -8.480771745766411129, -4.382649155111336903 ) ) ;
#2634=LINE ( 'NONE', #7250, #4394 ) ;
#2659=DIRECTION ( 'NONE',  ( 0.8660254037844382635, 0.5000000000000006661, 0.000000000000000000 ) ) ;
#2663=ORIENTED_EDGE ( 'NONE', *, *, #6365, .T. ) ;
#2672=ORIENTED_EDGE ( 'NONE', *, *, #362, .F. ) ;
#2673=ORIENTED_EDGE ( 'NONE', *, *, #4171, .T. ) ;
#2676=DIRECTION ( 'NONE',  ( -0.000000000000000000, -0.000000000000000000, -1.000000000000000000 ) ) ;
#2684=EDGE_CURVE ( 'NONE', #6492, #6903, #3013, .T. ) ;
#2685=EDGE_CURVE ( 'NONE', #2582, #1983, #295, .T. ) ;
#2705=CARTESIAN_POINT ( 'NONE',  ( 8.000000000000000000, 4.618802153517004072, -4.700000000000000178 ) ) ;
#2706=DIRECTION ( 'NONE',  ( -0.000000000000000000, -0.000000000000000000, 1.000000000000000000 ) ) ;
#2721=AXIS2_PLACEMENT_3D ( 'NONE', #2738, #2042, #6216 ) ;
#2727=CARTESIAN_POINT ( 'NONE',  ( -1.734723475976807094E-15, 9.237604307034017026, -0.7145311798163319628 ) ) ;
#2737=CARTESIAN_POINT ( 'NONE',  ( -4.681546503268407275E-16, 9.237604307034017026, -4.700000000000000178 ) ) ;
#2738=CARTESIAN_POINT ( 'NONE',  ( 0.000000000000000000, 0.000000000000000000, 0.000000000000000000 ) ) ;
#2741=B_SPLINE_CURVE_WITH_KNOTS ( 'NONE', 3,
 ( #236, #2028, #7345, #5014, #786, #7381, #6909, #4497 ),
 .UNSPECIFIED., .F., .F.,
 ( 4, 2, 2, 4 ),
 ( 0.004673709593152148775, 0.005837709341827643401, 0.007001709090503138028, 0.009329708587854127280 ),
 .UNSPECIFIED. ) ;
#2742=CARTESIAN_POINT ( 'NONE',  ( 0.000000000000000000, 0.000000000000000000, -4.699999999999999289 ) ) ;
#2746=CARTESIAN_POINT ( 'NONE',  ( 3.660532965668823469, -7.124194613927629760, -4.700000000000001066 ) ) ;
#2752=EDGE_CURVE ( 'NONE', #3955, #2329, #6898, .T. ) ;
#2778=FACE_OUTER_BOUND ( 'NONE', #5832, .T. ) ;
#2781=EDGE_CURVE ( 'NONE', #1722, #2329, #3901, .T. ) ;
#2794=DIRECTION ( 'NONE',  ( -0.000000000000000000, -0.000000000000000000, 1.000000000000000000 ) ) ;
#2816=CARTESIAN_POINT ( 'NONE',  ( 0.000000000000000000, 0.000000000000000000, -4.674599999999997202 ) ) ;
#2842=ORIENTED_EDGE ( 'NONE', *, *, #3985, .F. ) ;
#2846=CARTESIAN_POINT ( 'NONE',  ( 0.000000000000000000, 0.000000000000000000, 2.573333333333333695 ) ) ;
#2849=DIRECTION ( 'NONE',  ( 1.000000000000000000, 0.000000000000000000, 0.000000000000000000 ) ) ;
#2854=ORIENTED_EDGE ( 'NONE', *, *, #2781, .T. ) ;
#2864=ORIENTED_EDGE ( 'NONE', *, *, #6009, .T. ) ;
#2866=VERTEX_POINT ( 'NONE', #3736 ) ;
#2870=CARTESIAN_POINT ( 'NONE',  ( 8.000000000000000000, 4.618802153517013842, -0.7145311798163319628 ) ) ;
#2879=AXIS2_PLACEMENT_3D ( 'NONE', #5020, #4428, #1424 ) ;
#2881=CARTESIAN_POINT ( 'NONE',  ( -8.000000000000001776, -1.555946510856140996, -0.06708870216335509340 ) ) ;
#2897=CIRCLE ( 'NONE', #1376, 5.857142857142855874 ) ;
#2898=ORIENTED_EDGE ( 'NONE', *, *, #843, .F. ) ;
#2901=CIRCLE ( 'NONE', #9, 7.999999999999998224 ) ;
#2903=PLANE ( 'NONE',  #6906 ) ;
#2905=CARTESIAN_POINT ( 'NONE',  ( 0.000000000000000000, 0.000000000000000000, 2.573333333332999739 ) ) ;
#2910=CARTESIAN_POINT ( 'NONE',  ( -1.734723475976807094E-15, 9.237604307034017026, -3.985468820183668104 ) ) ;
#2911=DIRECTION ( 'NONE',  ( 1.000000000000000000, 0.000000000000000000, 0.000000000000000000 ) ) ;
#2918=VECTOR ( 'NONE', #5002, 1000.000000000000000 ) ;
#2921=FACE_BOUND ( 'NONE', #1159, .T. ) ;
#2924=EDGE_CURVE ( 'NONE', #4597, #926, #2897, .T. ) ;
#2946=DIRECTION ( 'NONE',  ( 1.000000000000000000, 0.000000000000000000, 0.000000000000000000 ) ) ;
#2951=CARTESIAN_POINT ( 'NONE',  ( -6.686525924292790357, 5.377136764700156668, -4.383279549040164369 ) ) ;
#2964=( LENGTH_UNIT ( ) NAMED_UNIT ( * ) SI_UNIT ( .MILLI., .METRE. ) );
#2984=ADVANCED_FACE ( 'NONE', ( #1923 ), #238, .T. ) ;
#2986=PRODUCT_DEFINITION_CONTEXT ( 'detailed design', #2040, 'design' ) ;
#2991=CARTESIAN_POINT ( 'NONE',  ( 5.355005115540896199, 6.145890662064656063, -4.617753204360287356 ) ) ;
#2997=CARTESIAN_POINT ( 'NONE',  ( 0.000000000000000000, 0.000000000000000000, 0.000000000000000000 ) ) ;
#2999=ORIENTED_EDGE ( 'NONE', *, *, #2924, .F. ) ;
#3002=ORIENTED_EDGE ( 'NONE', *, *, #3174, .F. ) ;
#3003=DIRECTION ( 'NONE',  ( 0.000000000000000000, 0.000000000000000000, -1.000000000000000000 ) ) ;
#3010=DIRECTION ( 'NONE',  ( -1.000000000000000000, 0.000000000000000000, 0.000000000000000000 ) ) ;
#3013=CIRCLE ( 'NONE', #7414, 4.250000000000000000 ) ;
#3024=ORIENTED_EDGE ( 'NONE', *, *, #3124, .F. ) ;
#3025=EDGE_CURVE ( 'NONE', #1610, #3551, #2634, .T. ) ;
#3044=CARTESIAN_POINT ( 'NONE',  ( 5.000000000000000888, 0.000000000000000000, 19.04999999999997229 ) ) ;
#3046=SURFACE_STYLE_USAGE ( .BOTH. , #4176 ) ;
#3052=CARTESIAN_POINT ( 'NONE',  ( -2.081668171172168513E-14, -9.237604307034017026, -0.7145311798163319628 ) ) ;
#3054=VERTEX_POINT ( 'NONE', #1818 ) ;
#3055=ORIENTED_EDGE ( 'NONE', *, *, #3850, .T. ) ;
#3061=FACE_BOUND ( 'NONE', #4149, .T. ) ;
#3074=ORIENTED_EDGE ( 'NONE', *, *, #7182, .F. ) ;
#3078=CARTESIAN_POINT ( 'NONE',  ( 7.345652830558762503, -4.996589667937383794, -4.203584543331203349 ) ) ;
#3080=DIRECTION ( 'NONE',  ( 0.8191520442889924647, 1.003171929053525486E-16, -0.5735764363510451602 ) ) ;
#3113=ORIENTED_EDGE ( 'NONE', *, *, #3122, .F. ) ;
#3114=ADVANCED_FACE ( 'NONE', ( #2921, #3588 ), #467, .F. ) ;
#3118=DIRECTION ( 'NONE',  ( -0.000000000000000000, -0.000000000000000000, 1.000000000000000000 ) ) ;
#3121=VERTEX_POINT ( 'NONE', #5997 ) ;
#3122=EDGE_CURVE ( 'NONE', #3787, #7537, #6174, .T. ) ;
#3124=EDGE_CURVE ( 'NONE', #5462, #7689, #4556, .T. ) ;
#3128=CARTESIAN_POINT ( 'NONE',  ( -8.000000000000000000, -4.618802153517013842, -3.985468820183668104 ) ) ;
#3131=CARTESIAN_POINT ( 'NONE',  ( 8.000000000000000000, -0.7805016046290993437, -4.700000000000000178 ) ) ;
#3138=CIRCLE ( 'NONE', #6788, 8.000000000000000000 ) ;
#3145=MANIFOLD_SOLID_BREP ( 'TorqueElement', #1452 ) ;
#3156=ORIENTED_EDGE ( 'NONE', *, *, #2312, .F. ) ;
#3157=CYLINDRICAL_SURFACE ( 'NONE', #16, 5.000000000000000888 ) ;
#3159=CONICAL_SURFACE ( 'NONE', #6930, 8.000000000000000000, 1.047197551196596299 ) ;
#3168=EDGE_CURVE ( 'NONE', #6375, #6313, #6911, .T. ) ;
#3174=EDGE_CURVE ( 'NONE', #544, #6148, #1001, .T. ) ;
#3175=ORIENTED_EDGE ( 'NONE', *, *, #1629, .F. ) ;
#3177=CARTESIAN_POINT ( 'NONE',  ( 0.000000000000000000, 0.000000000000000000, -4.674599999999997202 ) ) ;
#3208=VECTOR ( 'NONE', #5506, 1000.000000000000000 ) ;
#3209=CARTESIAN_POINT ( 'NONE',  ( -0.6527133886630326343, 8.860760056385741379, -0.4969600502617543270 ) ) ;
#3227=CARTESIAN_POINT ( 'NONE',  ( 0.6527133886630215320, -8.860760056385755590, -4.203039949738235137 ) ) ;
#3258=PRODUCT_CONTEXT ( 'NONE', #4595, 'mechanical' ) ;
#3259=AXIS2_PLACEMENT_3D ( 'NONE', #1281, #4279, #4795 ) ;
#3265=ORIENTED_EDGE ( 'NONE', *, *, #988, .F. ) ;
#3269=EDGE_CURVE ( 'NONE', #7689, #3301, #4933, .T. ) ;
#3283=ORIENTED_EDGE ( 'NONE', *, *, #176, .T. ) ;
#3289=DIRECTION ( 'NONE',  ( 1.000000000000000000, 0.000000000000000000, 0.000000000000000000 ) ) ;
#3301=VERTEX_POINT ( 'NONE', #338 ) ;
#3308=CONICAL_SURFACE ( 'NONE', #906, 5.000000000000000888, 0.9599310885968824758 ) ;
#3316=ADVANCED_FACE ( 'NONE', ( #930 ), #892, .F. ) ;
#3318=CARTESIAN_POINT ( 'NONE',  ( 1.313474075707211197, 8.479269695850863542, -0.3167204509598410267 ) ) ;
#3332=CARTESIAN_POINT ( 'NONE',  ( -8.000000000000000000, 0.000000000000000000, 0.000000000000000000 ) ) ;
#3338=CARTESIAN_POINT ( 'NONE',  ( 2.309976723937607890, -7.903938623646878270, -4.569346954796185578 ) ) ;
#3341=ORIENTED_EDGE ( 'NONE', *, *, #3168, .T. ) ;
#3345=CARTESIAN_POINT ( 'NONE',  ( 2.503857664561936813E-16, -9.237604307034025908, -4.700000000000000178 ) ) ;
#3354=DIRECTION ( 'NONE',  ( -0.000000000000000000, -0.000000000000000000, 1.000000000000000000 ) ) ;
#3357=EDGE_CURVE ( 'NONE', #406, #1868, #2901, .T. ) ;
#3359=ADVANCED_FACE ( 'NONE', ( #1489 ), #3159, .T. ) ;
#3366=CARTESIAN_POINT ( 'NONE',  ( -7.347286611336972584, -4.995646404165285936, -4.203039949738244019 ) ) ;
#3392=VERTEX_POINT ( 'NONE', #5925 ) ;
#3393=CARTESIAN_POINT ( 'NONE',  ( 0.000000000000000000, 0.000000000000000000, 2.573333333333333695 ) ) ;
#3400=DIRECTION ( 'NONE',  ( 0.5000000000000006661, -0.8660254037844382635, 0.000000000000000000 ) ) ;
#3412=ADVANCED_FACE ( 'NONE', ( #7145 ), #4026, .F. ) ;
#3419=CARTESIAN_POINT ( 'NONE',  ( 5.690023276062393442, 5.952467836904152598, -0.1306530452038090484 ) ) ;
#3422=CARTESIAN_POINT ( 'NONE',  ( -8.000000000000000000, -4.618802153517013842, -3.985468820183668104 ) ) ;
#3438=CARTESIAN_POINT ( 'NONE',  ( 0.000000000000000000, 0.000000000000000000, -4.674599999999997202 ) ) ;
#3456=CARTESIAN_POINT ( 'NONE',  ( -1.310872448937999035, 8.480771745766400471, -4.382649155111345785 ) ) ;
#3470=CARTESIAN_POINT ( 'NONE',  ( -8.000000000000000000, 4.618802153517013842, -3.985468820183668104 ) ) ;
#3487=CARTESIAN_POINT ( 'NONE',  ( -8.000000000000000000, -0.7805016046291017862, -4.700000000000000178 ) ) ;
#3494=ORIENTED_EDGE ( 'NONE', *, *, #4523, .T. ) ;
#3505=CIRCLE ( 'NONE', #850, 7.999999999999998224 ) ;
#3507=ADVANCED_FACE ( 'NONE', ( #4184 ), #5039, .T. ) ;
#3508=ORIENTED_EDGE ( 'NONE', *, *, #2752, .F. ) ;
#3515=VECTOR ( 'NONE', #6925, 1000.000000000000000 ) ;
#3521=CARTESIAN_POINT ( 'NONE',  ( -4.680456609903975718, -6.535341423375596648, -4.683111142572228047 ) ) ;
#3522=ORIENTED_EDGE ( 'NONE', *, *, #3025, .T. ) ;
#3523=EDGE_LOOP ( 'NONE', ( #6573, #6857, #6768 ) ) ;
#3531=CARTESIAN_POINT ( 'NONE',  ( 0.000000000000000000, 0.000000000000000000, -4.700000000000000178 ) ) ;
#3536=CARTESIAN_POINT ( 'NONE',  ( 0.000000000000000000, 0.000000000000000000, 0.000000000000000000 ) ) ;
#3537=CARTESIAN_POINT ( 'NONE',  ( 8.000000000000000000, 0.000000000000000000, 0.000000000000000000 ) ) ;
#3540=AXIS2_PLACEMENT_3D ( 'NONE', #6907, #6317, #900 ) ;
#3547=CARTESIAN_POINT ( 'NONE',  ( -8.000000000000000000, -0.7805016046290998988, -3.388131789017200740E-17 ) ) ;
#3551=VERTEX_POINT ( 'NONE', #6082 ) ;
#3556=DIRECTION ( 'NONE',  ( 0.000000000000000000, 0.000000000000000000, 1.000000000000000000 ) ) ;
#3576=CARTESIAN_POINT ( 'NONE',  ( -8.000000000000000000, 4.618802153517013842, -3.985468820183668104 ) ) ;
#3588=FACE_OUTER_BOUND ( 'NONE', #2391, .T. ) ;
#3597=DIRECTION ( 'NONE',  ( 0.000000000000000000, 0.000000000000000000, -1.000000000000000000 ) ) ;
#3610=CARTESIAN_POINT ( 'NONE',  ( 0.000000000000000000, 0.000000000000000000, -4.674599999999997202 ) ) ;
#3614=PLANE ( 'NONE',  #1834 ) ;
#3617=B_SPLINE_CURVE_WITH_KNOTS ( 'NONE', 3,
 ( #3840, #1506, #241, #5054, #3914, #2151 ),
 .UNSPECIFIED., .F., .F.,
 ( 4, 2, 4 ),
 ( 2.380731629812508987E-07, 0.002336973833157575484, 0.004673709593152171327 ),
 .UNSPECIFIED. ) ;
#3675=CARTESIAN_POINT ( 'NONE',  ( -4.000000000000004441, -6.928203230275506108, 0.000000000000000000 ) ) ;
#3682=DIRECTION ( 'NONE',  ( -1.000000000000000000, 0.000000000000000000, 0.000000000000000000 ) ) ;
#3686=ORIENTED_EDGE ( 'NONE', *, *, #4179, .T. ) ;
#3706=CARTESIAN_POINT ( 'NONE',  ( 8.000000000000000000, -4.618802153517011178, -0.7145311798163319628 ) ) ;
#3715=CARTESIAN_POINT ( 'NONE',  ( -8.000000000000001776, -3.098204225878176121, -4.384209322808125364 ) ) ;
#3716=AXIS2_PLACEMENT_3D ( 'NONE', #2905, #2199, #7042 ) ;
#3720=ORIENTED_EDGE ( 'NONE', *, *, #3122, .T. ) ;
#3736=CARTESIAN_POINT ( 'NONE',  ( -6.713333333332999864, 9.009318285727158319E-16, 3.859999999999999876 ) ) ;
#3743=CARTESIAN_POINT ( 'NONE',  ( 0.000000000000000000, 0.000000000000000000, -4.700000000000000178 ) ) ;
#3744=CARTESIAN_POINT ( 'NONE',  ( 8.000000000000000000, -4.618802153517011178, -3.985468820183668104 ) ) ;
#3746=PRESENTATION_STYLE_ASSIGNMENT (( #3046 ) ) ;
#3758=DIRECTION ( 'NONE',  ( 0.000000000000000000, 0.000000000000000000, 1.000000000000000000 ) ) ;
#3783=( NAMED_UNIT ( * ) SI_UNIT ( $, .STERADIAN. ) SOLID_ANGLE_UNIT ( ) );
#3787=VERTEX_POINT ( 'NONE', #3868 ) ;
#3796=CIRCLE ( 'NONE', #765, 8.000000000000000000 ) ;
#3798=ORIENTED_EDGE ( 'NONE', *, *, #5640, .F. ) ;
#3801=ADVANCED_FACE ( 'NONE', ( #4494 ), #1265, .T. ) ;
#3802=CARTESIAN_POINT ( 'NONE',  ( -3.319543390096037605, 7.321065037175422674, -0.01688885742776584376 ) ) ;
#3813=CARTESIAN_POINT ( 'NONE',  ( 8.000000000000000000, 0.000000000000000000, -4.700000000000000178 ) ) ;
#3818=ORIENTED_EDGE ( 'NONE', *, *, #4655, .F. ) ;
#3824=AXIS2_PLACEMENT_3D ( 'NONE', #3177, #91, #4903 ) ;
#3835=ORIENTED_EDGE ( 'NONE', *, *, #362, .T. ) ;
#3840=CARTESIAN_POINT ( 'NONE',  ( -2.081668171172168513E-14, -9.237604307034017026, -3.985468820183668104 ) ) ;
#3841=EDGE_CURVE ( 'NONE', #1983, #6200, #4984, .T. ) ;
#3850=EDGE_CURVE ( 'NONE', #3551, #4484, #3796, .T. ) ;
#3868=CARTESIAN_POINT ( 'NONE',  ( 5.857142857142856762, 0.000000000000000000, 2.573333333332999739 ) ) ;
#3870=DIRECTION ( 'NONE',  ( 1.000000000000000000, 0.000000000000000000, 0.000000000000000000 ) ) ;
#3890=CIRCLE ( 'NONE', #3259, 5.857142857142855874 ) ;
#3893=EDGE_LOOP ( 'NONE', ( #1151, #7214, #6669, #1960 ) ) ;
#3897=ORIENTED_EDGE ( 'NONE', *, *, #4850, .T. ) ;
#3898=DIRECTION ( 'NONE',  ( -0.000000000000000000, -0.000000000000000000, -1.000000000000000000 ) ) ;
#3901=CIRCLE ( 'NONE', #5281, 8.000000000000000000 ) ;
#3909=CARTESIAN_POINT ( 'NONE',  ( 0.000000000000000000, 0.000000000000000000, 2.573333333332999739 ) ) ;
#3913=CONICAL_SURFACE ( 'NONE', #6190, 8.000000000000000000, 1.047197551196596299 ) ;
#3914=CARTESIAN_POINT ( 'NONE',  ( -3.318518101603016746, -7.321656987762879432, -4.700000000000000178 ) ) ;
#3921=CARTESIAN_POINT ( 'NONE',  ( 5.857142857142855874, 0.000000000000000000, 3.859999999999999876 ) ) ;
#3922=FACE_BOUND ( 'NONE', #577, .T. ) ;
#3945=ADVANCED_FACE ( 'NONE', ( #6628 ), #3913, .T. ) ;
#3955=VERTEX_POINT ( 'NONE', #3706 ) ;
#3962=DIRECTION ( 'NONE',  ( 0.000000000000000000, 0.000000000000000000, -1.000000000000000000 ) ) ;
#3980=ADVANCED_FACE ( 'NONE', ( #6742 ), #2543, .T. ) ;
#3985=EDGE_CURVE ( 'NONE', #5419, #3392, #6111, .T. ) ;
#3990=CARTESIAN_POINT ( 'NONE',  ( -5.355005115540898863, -6.145890662064660503, -4.617753204360282915 ) ) ;
#4005=CARTESIAN_POINT ( 'NONE',  ( 4.680456609903971277, 6.535341423375591319, -4.683111142572234264 ) ) ;
#4018=AXIS2_PLACEMENT_3D ( 'NONE', #183, #5507, #6733 ) ;
#4022=ORIENTED_EDGE ( 'NONE', *, *, #2781, .F. ) ;
#4026=CYLINDRICAL_SURFACE ( 'NONE', #7190, 4.250000000000000000 ) ;
#4030=ORIENTED_EDGE ( 'NONE', *, *, #5811, .T. ) ;
#4031=ORIENTED_EDGE ( 'NONE', *, *, #6303, .F. ) ;
#4032=ADVANCED_FACE ( 'NONE', ( #4806 ), #3157, .F. ) ;
#4036=DIRECTION ( 'NONE',  ( 0.5000000000000006661, 0.8660254037844383745, -0.000000000000000000 ) ) ;
#4038=CARTESIAN_POINT ( 'NONE',  ( 0.000000000000000000, 0.000000000000000000, 0.000000000000000000 ) ) ;
#4050=ORIENTED_EDGE ( 'NONE', *, *, #4507, .F. ) ;
#4055=DIRECTION ( 'NONE',  ( -0.000000000000000000, -0.000000000000000000, 1.000000000000000000 ) ) ;
#4062=DIRECTION ( 'NONE',  ( 0.000000000000000000, 0.000000000000000000, 1.000000000000000000 ) ) ;
#4082=ORIENTED_EDGE ( 'NONE', *, *, #6879, .F. ) ;
#4083=CARTESIAN_POINT ( 'NONE',  ( -4.000000000000004441, 6.928203230275506108, 0.000000000000000000 ) ) ;
#4084=EDGE_CURVE ( 'NONE', #3054, #1983, #640, .T. ) ;
#4090=EDGE_LOOP ( 'NONE', ( #1402, #3897, #2218, #342 ) ) ;
#4093=VERTEX_POINT ( 'NONE', #1978 ) ;
#4094=CARTESIAN_POINT ( 'NONE',  ( -8.000000000000000000, 0.000000000000000000, -4.700000000000000178 ) ) ;
#4099=VECTOR ( 'NONE', #5102, 1000.000000000000000 ) ;
#4100=CARTESIAN_POINT ( 'NONE',  ( -2.081668171172168513E-14, -9.237604307034017026, -0.7145311798163319628 ) ) ;
#4111=CARTESIAN_POINT ( 'NONE',  ( -8.000000000000000000, 0.000000000000000000, -4.700000000000000178 ) ) ;
#4116=VERTEX_POINT ( 'NONE', #5115 ) ;
#4122=CYLINDRICAL_SURFACE ( 'NONE', #4892, 5.857142857142855874 ) ;
#4127=AXIS2_PLACEMENT_3D ( 'NONE', #5415, #4854, #7344 ) ;
#4128=ADVANCED_FACE ( 'NONE', ( #1527 ), #6191, .T. ) ;
#4147=ORIENTED_EDGE ( 'NONE', *, *, #426, .T. ) ;
#4149=EDGE_LOOP ( 'NONE', ( #4848, #504 ) ) ;
#4162=CARTESIAN_POINT ( 'NONE',  ( 7.347286611336970807, 4.995646404165279719, -4.203039949738250236 ) ) ;
#4163=LINE ( 'NONE', #4204, #1882 ) ;
#4171=EDGE_CURVE ( 'NONE', #7537, #926, #776, .T. ) ;
#4173=CARTESIAN_POINT ( 'NONE',  ( -8.000000000000000000, 3.871967595402128648, -4.201061386767543482 ) ) ;
#4174=DIRECTION ( 'NONE',  ( -0.000000000000000000, -0.000000000000000000, 1.000000000000000000 ) ) ;
#4176=SURFACE_SIDE_STYLE ('',( #5408 ) ) ;
#4177=EDGE_CURVE ( 'NONE', #5419, #115, #2295, .T. ) ;
#4179=EDGE_CURVE ( 'NONE', #1026, #980, #4486, .T. ) ;
#4184=FACE_OUTER_BOUND ( 'NONE', #5781, .T. ) ;
#4204=CARTESIAN_POINT ( 'NONE',  ( -5.000000000000000888, 0.000000000000000000, -4.674599999999997202 ) ) ;
#4217=AXIS2_PLACEMENT_3D ( 'NONE', #3531, #532, #2946 ) ;
#4220=EDGE_LOOP ( 'NONE', ( #3283, #1893, #5961 ) ) ;
#4232=PLANE ( 'NONE',  #4960 ) ;
#4236=UNCERTAINTY_MEASURE_WITH_UNIT (LENGTH_MEASURE( 1.000000000000000082E-05 ), #6039, 'distance_accuracy_value', 'NONE');
#4246=DIRECTION ( 'NONE',  ( -0.000000000000000000, -0.000000000000000000, 1.000000000000000000 ) ) ;
#4248=ORIENTED_EDGE ( 'NONE', *, *, #1747, .T. ) ;
#4255=CARTESIAN_POINT ( 'NONE',  ( -8.000000000000000000, -4.618802153517013842, -0.7145311798163319628 ) ) ;
#4257=VERTEX_POINT ( 'NONE', #2134 ) ;
#4262=CARTESIAN_POINT ( 'NONE',  ( -2.645508037661889134, -7.710219529346611367, -0.06809871960543237290 ) ) ;
#4278=EDGE_CURVE ( 'NONE', #3955, #1610, #4704, .T. ) ;
#4279=DIRECTION ( 'NONE',  ( -0.000000000000000000, -0.000000000000000000, 1.000000000000000000 ) ) ;
#4288=ADVANCED_FACE ( 'NONE', ( #5903 ), #4122, .F. ) ;
#4301=DIRECTION ( 'NONE',  ( -0.000000000000000000, -0.000000000000000000, -1.000000000000000000 ) ) ;
#4303=ORIENTED_EDGE ( 'NONE', *, *, #2219, .F. ) ;
#4310=CARTESIAN_POINT ( 'NONE',  ( 0.000000000000000000, 4.250000000000000000, 2.573333333332999739 ) ) ;
#4312=ADVANCED_FACE ( 'NONE', ( #6538 ), #1604, .F. ) ;
#4315=EDGE_CURVE ( 'NONE', #2582, #5462, #1684, .T. ) ;
#4327=EDGE_CURVE ( 'NONE', #4116, #2529, #474, .T. ) ;
#4373=ORIENTED_EDGE ( 'NONE', *, *, #6890, .T. ) ;
#4394=VECTOR ( 'NONE', #4246, 1000.000000000000000 ) ;
#4405=DIRECTION ( 'NONE',  ( 0.000000000000000000, 0.000000000000000000, 1.000000000000000000 ) ) ;
#4413=EDGE_LOOP ( 'NONE', ( #6261, #3175, #381, #1520, #812, #6225 ) ) ;
#4428=DIRECTION ( 'NONE',  ( 0.000000000000000000, 0.000000000000000000, -1.000000000000000000 ) ) ;
#4430=B_SPLINE_CURVE_WITH_KNOTS ( 'NONE', 3,
 ( #2248, #6535, #536, #410, #2286, #4083 ),
 .UNSPECIFIED., .F., .F.,
 ( 4, 2, 4 ),
 ( 2.380731629582122378E-07, 0.002336973833157555969, 0.004673709593152153112 ),
 .UNSPECIFIED. ) ;
#4431=ORIENTED_EDGE ( 'NONE', *, *, #4177, .F. ) ;
#4484=VERTEX_POINT ( 'NONE', #691 ) ;
#4486=LINE ( 'NONE', #3345, #4671 ) ;
#4493=ORIENTED_EDGE ( 'NONE', *, *, #3841, .F. ) ;
#4494=FACE_OUTER_BOUND ( 'NONE', #6042, .T. ) ;
#4497=CARTESIAN_POINT ( 'NONE',  ( -2.081668171172168513E-14, -9.237604307034017026, -0.7145311798163319628 ) ) ;
#4507=EDGE_CURVE ( 'NONE', #926, #4597, #3890, .T. ) ;
#4509=AXIS2_PLACEMENT_3D ( 'NONE', #7462, #5764, #276 ) ;
#4523=EDGE_CURVE ( 'NONE', #6148, #7619, #4163, .T. ) ;
#4533=ORIENTED_EDGE ( 'NONE', *, *, #2539, .F. ) ;
#4546=CARTESIAN_POINT ( 'NONE',  ( -4.000000000000004441, 6.928203230275506108, -4.700000000000000178 ) ) ;
#4556=B_SPLINE_CURVE_WITH_KNOTS ( 'NONE', 3,
 ( #591, #6586, #1176, #2881, #3547, #7717 ),
 .UNSPECIFIED., .F., .F.,
 ( 4, 2, 4 ),
 ( 0.008240550023493525833, 0.01057684187039405199, 0.01291313371729457642 ),
 .UNSPECIFIED. ) ;
#4563=CARTESIAN_POINT ( 'NONE',  ( -8.000000000000000000, 3.871967595402119766, -0.4989386132324563627 ) ) ;
#4575=CARTESIAN_POINT ( 'NONE',  ( 2.645508037661878475, 7.710219529346607814, -0.06809871960542819569 ) ) ;
#4590=CARTESIAN_POINT ( 'NONE',  ( 0.000000000000000000, 5.857142857142855874, 3.859999999999999876 ) ) ;
#4595=APPLICATION_CONTEXT ( 'automotive_design' ) ;
#4597=VERTEX_POINT ( 'NONE', #3921 ) ;
#4601=CARTESIAN_POINT ( 'NONE',  ( -7.345652830558756285, 4.996589667937373136, -4.203584543331207790 ) ) ;
#4615=LINE ( 'NONE', #4688, #7726 ) ;
#4628=DIRECTION ( 'NONE',  ( 1.000000000000000000, 0.000000000000000000, 0.000000000000000000 ) ) ;
#4639=CARTESIAN_POINT ( 'NONE',  ( 8.000000000000000000, 4.618802153517013842, -3.985468820183668104 ) ) ;
#4640=AXIS2_PLACEMENT_3D ( 'NONE', #1644, #1087, #7674 ) ;
#4646=ORIENTED_EDGE ( 'NONE', *, *, #4179, .F. ) ;
#4652=FACE_OUTER_BOUND ( 'NONE', #7428, .T. ) ;
#4653=EDGE_CURVE ( 'NONE', #4093, #2529, #919, .T. ) ;
#4655=EDGE_CURVE ( 'NONE', #1789, #4093, #5163, .T. ) ;
#4657=ADVANCED_FACE ( 'NONE', ( #6811 ), #2082, .F. ) ;
#4664=EDGE_LOOP ( 'NONE', ( #5740, #3074, #3508 ) ) ;
#4671=VECTOR ( 'NONE', #4405, 1000.000000000000000 ) ;
#4676=CARTESIAN_POINT ( 'NONE',  ( -8.000000000000000000, -4.618802153517012954, -4.700000000000000178 ) ) ;
#4681=ORIENTED_EDGE ( 'NONE', *, *, #125, .T. ) ;
#4688=CARTESIAN_POINT ( 'NONE',  ( -4.681546503268407275E-16, 9.237604307034017026, -4.700000000000000178 ) ) ;
#4691=EDGE_LOOP ( 'NONE', ( #1442, #3002, #2663, #2864 ) ) ;
#4694=CARTESIAN_POINT ( 'NONE',  ( 0.000000000000000000, 0.000000000000000000, 0.000000000000000000 ) ) ;
#4698=CARTESIAN_POINT ( 'NONE',  ( -5.690023276062397883, -5.952467836904158816, -4.569346954796184690 ) ) ;
#4704=B_SPLINE_CURVE_WITH_KNOTS ( 'NONE', 3,
 ( #1565, #6971, #537, #5270, #1732, #3537 ),
 .UNSPECIFIED., .F., .F.,
 ( 4, 2, 4 ),
 ( 0.008240550023493527568, 0.01057684187039405199, 0.01291313371729457642 ),
 .UNSPECIFIED. ) ;
#4721=DIRECTION ( 'NONE',  ( 1.000000000000000000, 0.000000000000000000, 0.000000000000000000 ) ) ;
#4751=ORIENTED_EDGE ( 'NONE', *, *, #5439, .T. ) ;
#4787=DIRECTION ( 'NONE',  ( 0.000000000000000000, 0.000000000000000000, 1.000000000000000000 ) ) ;
#4795=DIRECTION ( 'NONE',  ( 1.000000000000000000, 0.000000000000000000, 0.000000000000000000 ) ) ;
#4796=DIRECTION ( 'NONE',  ( 1.000000000000000000, 0.000000000000000000, 0.000000000000000000 ) ) ;
#4806=FACE_OUTER_BOUND ( 'NONE', #4090, .T. ) ;
#4808=DIRECTION ( 'NONE',  ( -0.000000000000000000, -0.000000000000000000, 1.000000000000000000 ) ) ;
#4812=AXIS2_PLACEMENT_3D ( 'NONE', #5577, #796, #5615 ) ;
#4817=B_SPLINE_CURVE_WITH_KNOTS ( 'NONE', 3,
 ( #1388, #7533, #3802, #6204, #790, #5647, #3209, #5612 ),
 .UNSPECIFIED., .F., .F.,
 ( 4, 2, 2, 4 ),
 ( 0.004673709593152153112, 0.005837709341827643401, 0.007001709090503132824, 0.009329708587854111668 ),
 .UNSPECIFIED. ) ;
#4826=DIRECTION ( 'NONE',  ( 1.000000000000000000, 0.000000000000000000, 0.000000000000000000 ) ) ;
#4838=ORIENTED_EDGE ( 'NONE', *, *, #6365, .F. ) ;
#4839=ORIENTED_EDGE ( 'NONE', *, *, #1344, .F. ) ;
#4844=CARTESIAN_POINT ( 'NONE',  ( 4.000000000000005329, -6.928203230275506108, -4.700000000000000178 ) ) ;
#4848=ORIENTED_EDGE ( 'NONE', *, *, #6009, .F. ) ;
#4850=EDGE_CURVE ( 'NONE', #115, #5419, #1766, .T. ) ;
#4854=DIRECTION ( 'NONE',  ( -0.000000000000000000, -0.000000000000000000, 1.000000000000000000 ) ) ;
#4856=EDGE_LOOP ( 'NONE', ( #7611, #4751, #7649, #1101 ) ) ;
#4859=VERTEX_POINT ( 'NONE', #5262 ) ;
#4880=EDGE_LOOP ( 'NONE', ( #4681, #4533, #2103 ) ) ;
#4883=DIRECTION ( 'NONE',  ( 1.000000000000000000, 0.000000000000000000, 0.000000000000000000 ) ) ;
#4884=( NAMED_UNIT ( * ) SI_UNIT ( $, .STERADIAN. ) SOLID_ANGLE_UNIT ( ) );
#4892=AXIS2_PLACEMENT_3D ( 'NONE', #5310, #2249, #2911 ) ;
#4894=CARTESIAN_POINT ( 'NONE',  ( -3.318518101603016746, -7.321656987762879432, -1.128247885742728249E-15 ) ) ;
#4903=DIRECTION ( 'NONE',  ( -1.000000000000000000, 0.000000000000000000, 0.000000000000000000 ) ) ;
#4929=CARTESIAN_POINT ( 'NONE',  ( -8.000000000000001776, -1.555946510856144105, -4.632911297836646014 ) ) ;
#4932=ORIENTED_EDGE ( 'NONE', *, *, #1778, .T. ) ;
#4933=B_SPLINE_CURVE_WITH_KNOTS ( 'NONE', 3,
 ( #6383, #6268, #300, #2135, #4563, #1566 ),
 .UNSPECIFIED., .F., .F.,
 ( 4, 2, 4 ),
 ( 0.01291313371729457642, 0.01525081363757308656, 0.01758849355785159843 ),
 .UNSPECIFIED. ) ;
#4952=DIRECTION ( 'NONE',  ( -0.000000000000000000, -0.000000000000000000, 1.000000000000000000 ) ) ;
#4960=AXIS2_PLACEMENT_3D ( 'NONE', #6646, #3400, #2659 ) ;
#4961=DIRECTION ( 'NONE',  ( 1.000000000000000000, 0.000000000000000000, 0.000000000000000000 ) ) ;
#4984=B_SPLINE_CURVE_WITH_KNOTS ( 'NONE', 3,
 ( #4094, #7762, #7722, #2258, #4173, #3470 ),
 .UNSPECIFIED., .F., .F.,
 ( 4, 2, 4 ),
 ( 0.01291313371729457642, 0.01525081363757309350, 0.01758849355785161231 ),
 .UNSPECIFIED. ) ;
#4998=ORIENTED_EDGE ( 'NONE', *, *, #6740, .F. ) ;
#5002=DIRECTION ( 'NONE',  ( -0.000000000000000000, -0.000000000000000000, 1.000000000000000000 ) ) ;
#5014=CARTESIAN_POINT ( 'NONE',  ( 2.644994884459109574, -7.710515798486373029, -0.08224679563971952490 ) ) ;
#5019=FACE_OUTER_BOUND ( 'NONE', #2454, .T. ) ;
#5020=CARTESIAN_POINT ( 'NONE',  ( 0.000000000000000000, 0.000000000000000000, 0.000000000000000000 ) ) ;
#5034=MECHANICAL_DESIGN_GEOMETRIC_PRESENTATION_REPRESENTATION('',(#6178),#1384);
#5037=CARTESIAN_POINT ( 'NONE',  ( 0.000000000000000000, 0.000000000000000000, -4.699999999999999289 ) ) ;
#5039=CONICAL_SURFACE ( 'NONE', #2034, 8.000000000000000000, 1.047197551196596299 ) ;
#5047=EDGE_CURVE ( 'NONE', #4257, #7689, #2144, .T. ) ;
#5054=CARTESIAN_POINT ( 'NONE',  ( -2.645508037661888689, -7.710219529346611367, -4.631901280394566278 ) ) ;
#5059=DIRECTION ( 'NONE',  ( -0.5000000000000006661, 0.8660254037844383745, 0.000000000000000000 ) ) ;
#5061=CIRCLE ( 'NONE', #5566, 7.999999999999998224 ) ;
#5065=CARTESIAN_POINT ( 'NONE',  ( 2.644994884459109574, -7.710515798486373029, -4.617753204360279362 ) ) ;
#5084=CIRCLE ( 'NONE', #2200, 8.000000000000000000 ) ;
#5098=ADVANCED_FACE ( 'NONE', ( #5716 ), #1118, .T. ) ;
#5102=DIRECTION ( 'NONE',  ( -0.000000000000000000, -0.000000000000000000, 1.000000000000000000 ) ) ;
#5106=CARTESIAN_POINT ( 'NONE',  ( 0.000000000000000000, 0.000000000000000000, 3.859999999999999876 ) ) ;
#5115=CARTESIAN_POINT ( 'NONE',  ( 4.000000000000004441, 6.928203230275507885, 0.000000000000000000 ) ) ;
#5124=DIRECTION ( 'NONE',  ( 1.000000000000000000, 0.000000000000000000, 0.000000000000000000 ) ) ;
#5134=AXIS2_PLACEMENT_3D ( 'NONE', #1225, #4301, #6709 ) ;
#5138=PLANE ( 'NONE',  #6011 ) ;
#5162=DIRECTION ( 'NONE',  ( 0.000000000000000000, 0.000000000000000000, 1.000000000000000000 ) ) ;
#5163=B_SPLINE_CURVE_WITH_KNOTS ( 'NONE', 3,
 ( #2562, #5542, #844, #2125, #142, #177 ),
 .UNSPECIFIED., .F., .F.,
 ( 4, 2, 4 ),
 ( 0.01291313371729457815, 0.01525081363757309523, 0.01758849355785161231 ),
 .UNSPECIFIED. ) ;
#5164=DIRECTION ( 'NONE',  ( -0.000000000000000000, -0.000000000000000000, 1.000000000000000000 ) ) ;
#5170=CARTESIAN_POINT ( 'NONE',  ( 0.6543471694412381634, 8.859816792613644409, -4.203584543331201573 ) ) ;
#5191=DIRECTION ( 'NONE',  ( 0.000000000000000000, 0.000000000000000000, 1.000000000000000000 ) ) ;
#5192=CARTESIAN_POINT ( 'NONE',  ( 0.000000000000000000, 0.000000000000000000, -4.700000000000000178 ) ) ;
#5206=CARTESIAN_POINT ( 'NONE',  ( 4.250000000000000000, 0.000000000000000000, 2.573333333332999739 ) ) ;
#5220=CARTESIAN_POINT ( 'NONE',  ( -4.000000000000004441, -6.928203230275506108, 0.000000000000000000 ) ) ;
#5229=ORIENTED_EDGE ( 'NONE', *, *, #2219, .T. ) ;
#5231=FACE_OUTER_BOUND ( 'NONE', #5265, .T. ) ;
#5235=FACE_OUTER_BOUND ( 'NONE', #4880, .T. ) ;
#5236=CARTESIAN_POINT ( 'NONE',  ( 0.000000000000000000, 0.000000000000000000, 2.573333333332999739 ) ) ;
#5242=CIRCLE ( 'NONE', #2721, 8.000000000000000000 ) ;
#5262=CARTESIAN_POINT ( 'NONE',  ( 6.713333333332999864, 0.000000000000000000, 3.859999999999999876 ) ) ;
#5265=EDGE_LOOP ( 'NONE', ( #6640, #6262, #7403 ) ) ;
#5270=CARTESIAN_POINT ( 'NONE',  ( 8.000000000000000000, -1.555946510856141884, -0.06708870216335505177 ) ) ;
#5271=DIRECTION ( 'NONE',  ( -0.000000000000000000, -0.000000000000000000, 1.000000000000000000 ) ) ;
#5274=DIRECTION ( 'NONE',  ( -0.000000000000000000, -0.000000000000000000, 1.000000000000000000 ) ) ;
#5281=AXIS2_PLACEMENT_3D ( 'NONE', #2997, #5399, #5907 ) ;
#5289=CARTESIAN_POINT ( 'NONE',  ( 0.000000000000000000, 0.000000000000000000, -4.700000000000000178 ) ) ;
#5305=AXIS2_PLACEMENT_3D ( 'NONE', #3743, #2571, #4961 ) ;
#5310=CARTESIAN_POINT ( 'NONE',  ( 0.000000000000000000, 0.000000000000000000, 9.480888224575629408 ) ) ;
#5315=ORIENTED_EDGE ( 'NONE', *, *, #5439, .F. ) ;
#5319=DIRECTION ( 'NONE',  ( 1.000000000000000000, 0.000000000000000000, -0.000000000000000000 ) ) ;
#5323=EDGE_CURVE ( 'NONE', #5752, #3121, #4615, .T. ) ;
#5331=CARTESIAN_POINT ( 'NONE',  ( -1.734723475976807094E-15, 9.237604307034017026, -3.985468820183668104 ) ) ;
#5332=AXIS2_PLACEMENT_3D ( 'NONE', #3610, #2794, #1839 ) ;
#5344=DIRECTION ( 'NONE',  ( -0.8660254037844382635, 0.5000000000000005551, 0.000000000000000000 ) ) ;
#5348=AXIS2_PLACEMENT_3D ( 'NONE', #7132, #457, #7637 ) ;
#5366=CARTESIAN_POINT ( 'NONE',  ( -15.99999999999998934, -6.071532165918824830E-15, -4.700000000000000178 ) ) ;
#5372=DIRECTION ( 'NONE',  ( 1.000000000000000000, 0.000000000000000000, 0.000000000000000000 ) ) ;
#5382=CARTESIAN_POINT ( 'NONE',  ( 0.000000000000000000, 0.000000000000000000, 0.000000000000000000 ) ) ;
#5383=EDGE_CURVE ( 'NONE', #4859, #2866, #5838, .T. ) ;
#5389=DIRECTION ( 'NONE',  ( -1.000000000000000000, 0.000000000000000000, -0.000000000000000000 ) ) ;
#5393=CARTESIAN_POINT ( 'NONE',  ( -5.000000000000000888, 6.123233995736767268E-16, -4.699999999999999289 ) ) ;
#5399=DIRECTION ( 'NONE',  ( 0.000000000000000000, 0.000000000000000000, 1.000000000000000000 ) ) ;
#5400=TOROIDAL_SURFACE ( 'NONE', #4127, 6.713333333332999864, 1.286666666666999914 ) ;
#5406=DIRECTION ( 'NONE',  ( -1.000000000000000000, 0.000000000000000000, 0.000000000000000000 ) ) ;
#5408=SURFACE_STYLE_FILL_AREA ( #6113 ) ;
#5413=AXIS2_PLACEMENT_3D ( 'NONE', #7139, #4174, #2342 ) ;
#5415=CARTESIAN_POINT ( 'NONE',  ( 0.000000000000000000, 0.000000000000000000, 2.573333333332999739 ) ) ;
#5419=VERTEX_POINT ( 'NONE', #6745 ) ;
#5439=EDGE_CURVE ( 'NONE', #544, #3392, #2496, .T. ) ;
#5441=CARTESIAN_POINT ( 'NONE',  ( 0.000000000000000000, 0.000000000000000000, 0.000000000000000000 ) ) ;
#5445=ORIENTED_EDGE ( 'NONE', *, *, #2259, .F. ) ;
#5451=AXIS2_PLACEMENT_3D ( 'NONE', #2846, #5164, #2182 ) ;
#5457=CIRCLE ( 'NONE', #7350, 8.000000000000000000 ) ;
#5462=VERTEX_POINT ( 'NONE', #4255 ) ;
#5476=CARTESIAN_POINT ( 'NONE',  ( 0.000000000000000000, 0.000000000000000000, -4.149444346342716194 ) ) ;
#5506=DIRECTION ( 'NONE',  ( 0.000000000000000000, 0.000000000000000000, 1.000000000000000000 ) ) ;
#5507=DIRECTION ( 'NONE',  ( -0.000000000000000000, -0.000000000000000000, 1.000000000000000000 ) ) ;
#5519=ORIENTED_EDGE ( 'NONE', *, *, #2685, .F. ) ;
#5524=VECTOR ( 'NONE', #5191, 1000.000000000000000 ) ;
#5525=FACE_OUTER_BOUND ( 'NONE', #3893, .T. ) ;
#5527=ORIENTED_EDGE ( 'NONE', *, *, #843, .T. ) ;
#5529=AXIS2_PLACEMENT_3D ( 'NONE', #1459, #3354, #5124 ) ;
#5536=DIRECTION ( 'NONE',  ( 0.000000000000000000, 0.000000000000000000, -1.000000000000000000 ) ) ;
#5542=CARTESIAN_POINT ( 'NONE',  ( 8.000000000000000000, 0.7809653281576058870, -4.700000000000001066 ) ) ;
#5566=AXIS2_PLACEMENT_3D ( 'NONE', #873, #762, #3289 ) ;
#5577=CARTESIAN_POINT ( 'NONE',  ( 0.000000000000000000, 0.000000000000000000, -4.149444346342716194 ) ) ;
#5580=B_SPLINE_CURVE_WITH_KNOTS ( 'NONE', 3,
 ( #5331, #5170, #2268, #1022, #5884, #7573 ),
 .UNSPECIFIED., .F., .F.,
 ( 4, 2, 4 ),
 ( 2.380731629562773498E-07, 0.002336973833157560305, 0.004673709593152164388 ),
 .UNSPECIFIED. ) ;
#5602=ORIENTED_EDGE ( 'NONE', *, *, #4653, .F. ) ;
#5612=CARTESIAN_POINT ( 'NONE',  ( -1.734723475976807094E-15, 9.237604307034017026, -0.7145311798163319628 ) ) ;
#5614=FACE_OUTER_BOUND ( 'NONE', #4664, .T. ) ;
#5615=DIRECTION ( 'NONE',  ( -1.000000000000000000, 0.000000000000000000, 0.000000000000000000 ) ) ;
#5623=LINE ( 'NONE', #2630, #6773 ) ;
#5640=EDGE_CURVE ( 'NONE', #7689, #1722, #5084, .T. ) ;
#5647=CARTESIAN_POINT ( 'NONE',  ( -1.310872448937997925, 8.480771745766398695, -0.3173508448886566136 ) ) ;
#5652=AXIS2_PLACEMENT_3D ( 'NONE', #1578, #5162, #3870 ) ;
#5656=ADVANCED_FACE ( 'NONE', ( #5235 ), #1694, .T. ) ;
#5658=FACE_OUTER_BOUND ( 'NONE', #2350, .T. ) ;
#5688=CARTESIAN_POINT ( 'NONE',  ( 8.000000000000000000, -4.618802153517011178, -3.985468820183668104 ) ) ;
#5693=DIRECTION ( 'NONE',  ( -1.000000000000000000, 0.000000000000000000, 0.000000000000000000 ) ) ;
#5696=ORIENTED_EDGE ( 'NONE', *, *, #3269, .T. ) ;
#5699=AXIS2_PLACEMENT_3D ( 'NONE', #3909, #4055, #5758 ) ;
#5700=AXIS2_PLACEMENT_3D ( 'NONE', #723, #6093, #2552 ) ;
#5704=CARTESIAN_POINT ( 'NONE',  ( 0.000000000000000000, 0.000000000000000000, 0.000000000000000000 ) ) ;
#5716=FACE_OUTER_BOUND ( 'NONE', #4220, .T. ) ;
#5728=ORIENTED_EDGE ( 'NONE', *, *, #3850, .F. ) ;
#5731=DIRECTION ( 'NONE',  ( 1.224646799147353207E-16, 1.000000000000000000, 0.000000000000000000 ) ) ;
#5735=CARTESIAN_POINT ( 'NONE',  ( -4.000000000000004441, -6.928203230275506108, 0.000000000000000000 ) ) ;
#5740=ORIENTED_EDGE ( 'NONE', *, *, #4278, .T. ) ;
#5747=CARTESIAN_POINT ( 'NONE',  ( 0.000000000000000000, 0.000000000000000000, -4.700000000000000178 ) ) ;
#5752=VERTEX_POINT ( 'NONE', #6622 ) ;
#5754=B_SPLINE_CURVE_WITH_KNOTS ( 'NONE', 3,
 ( #5220, #7072, #2192, #2273, #7621, #485, #1670, #6996 ),
 .UNSPECIFIED., .F., .F.,
 ( 4, 2, 2, 4 ),
 ( 0.004673709593152171327, 0.005837709341827658147, 0.007001709090503144967, 0.009329708587854113402 ),
 .UNSPECIFIED. ) ;
#5758=DIRECTION ( 'NONE',  ( 1.000000000000000000, 0.000000000000000000, 0.000000000000000000 ) ) ;
#5759=ORIENTED_EDGE ( 'NONE', *, *, #125, .F. ) ;
#5760=CIRCLE ( 'NONE', #5700, 1.286666666666999914 ) ;
#5764=DIRECTION ( 'NONE',  ( -0.000000000000000000, -0.000000000000000000, 1.000000000000000000 ) ) ;
#5770=CYLINDRICAL_SURFACE ( 'NONE', #7013, 8.000000000000000000 ) ;
#5774=DIRECTION ( 'NONE',  ( -0.000000000000000000, -0.000000000000000000, 1.000000000000000000 ) ) ;
#5781=EDGE_LOOP ( 'NONE', ( #7177, #2133, #1669 ) ) ;
#5782=EDGE_CURVE ( 'NONE', #6148, #6492, #6103, .T. ) ;
#5784=ORIENTED_EDGE ( 'NONE', *, *, #6496, .F. ) ;
#5806=DIRECTION ( 'NONE',  ( 0.000000000000000000, 0.000000000000000000, -1.000000000000000000 ) ) ;
#5811=EDGE_CURVE ( 'NONE', #6313, #1026, #2112, .T. ) ;
#5824=CARTESIAN_POINT ( 'NONE',  ( 5.690023276062392554, 5.952467836904153486, -4.569346954796190907 ) ) ;
#5832=EDGE_LOOP ( 'NONE', ( #7210, #2108, #2854, #438, #3522, #4082 ) ) ;
#5838=CIRCLE ( 'NONE', #922, 6.713333333332999864 ) ;
#5848=CIRCLE ( 'NONE', #3716, 4.250000000000000000 ) ;
#5857=DIRECTION ( 'NONE',  ( 1.000000000000000000, 0.000000000000000000, 0.000000000000000000 ) ) ;
#5864=VECTOR ( 'NONE', #1603, 1000.000000000000000 ) ;
#5865=CARTESIAN_POINT ( 'NONE',  ( -0.6527133886630329673, 8.860760056385741379, -4.203039949738246683 ) ) ;
#5882=CARTESIAN_POINT ( 'NONE',  ( -5.857142857142855874, 7.172931252148781134E-16, 3.859999999999999876 ) ) ;
#5884=CARTESIAN_POINT ( 'NONE',  ( 3.318518101603008308, 7.321656987762871438, -4.700000000000006395 ) ) ;
#5891=CARTESIAN_POINT ( 'NONE',  ( 8.000000000000000000, 0.000000000000000000, 0.000000000000000000 ) ) ;
#5893=CARTESIAN_POINT ( 'NONE',  ( 4.000000000000004441, 6.928203230275507885, -4.700000000000000178 ) ) ;
#5901=CARTESIAN_POINT ( 'NONE',  ( -8.000000000000000000, 9.797174393178825657E-16, 9.480888224575629408 ) ) ;
#5903=FACE_OUTER_BOUND ( 'NONE', #543, .T. ) ;
#5907=DIRECTION ( 'NONE',  ( 1.000000000000000000, 0.000000000000000000, 0.000000000000000000 ) ) ;
#5910=ORIENTED_EDGE ( 'NONE', *, *, #2077, .F. ) ;
#5923=ADVANCED_FACE ( 'NONE', ( #1720 ), #1700, .T. ) ;
#5925=CARTESIAN_POINT ( 'NONE',  ( 5.000000000000000888, 6.123233995736767268E-16, -4.674599999999997202 ) ) ;
#5933=VECTOR ( 'NONE', #1255, 1000.000000000000000 ) ;
#5938=FACE_OUTER_BOUND ( 'NONE', #1836, .T. ) ;
#5942=B_SPLINE_CURVE_WITH_KNOTS ( 'NONE', 3,
 ( #831, #124, #2581, #716, #3131, #1342 ),
 .UNSPECIFIED., .F., .F.,
 ( 4, 2, 4 ),
 ( 0.008240550023493527568, 0.01057684187039405373, 0.01291313371729457815 ),
 .UNSPECIFIED. ) ;
#5957=PRODUCT_DEFINITION_FORMATION_WITH_SPECIFIED_SOURCE ( 'ANY', '', #1837, .NOT_KNOWN. ) ;
#5961=ORIENTED_EDGE ( 'NONE', *, *, #3357, .F. ) ;
#5977=DIRECTION ( 'NONE',  ( 1.000000000000000000, 0.000000000000000000, 0.000000000000000000 ) ) ;
#5985=CARTESIAN_POINT ( 'NONE',  ( -3.319543390096037161, 7.321065037175422674, -4.683111142572233376 ) ) ;
#5997=CARTESIAN_POINT ( 'NONE',  ( -1.734723475976807094E-15, 9.237604307034017026, -0.7145311798163319628 ) ) ;
#6009=EDGE_CURVE ( 'NONE', #6903, #6492, #5848, .T. ) ;
#6010=EDGE_LOOP ( 'NONE', ( #3686, #6723, #6287, #1899, #5784, #4303 ) ) ;
#6011=AXIS2_PLACEMENT_3D ( 'NONE', #2737, #5059, #174 ) ;
#6018=CIRCLE ( 'NONE', #2618, 6.713333333332999864 ) ;
#6022=ADVANCED_FACE ( 'NONE', ( #5938 ), #7707, .T. ) ;
#6026=DIRECTION ( 'NONE',  ( -0.8191520442889924647, 0.000000000000000000, -0.5735764363510451602 ) ) ;
#6039=( LENGTH_UNIT ( ) NAMED_UNIT ( * ) SI_UNIT ( .MILLI., .METRE. ) );
#6042=EDGE_LOOP ( 'NONE', ( #3341, #2221, #4998 ) ) ;
#6056=CARTESIAN_POINT ( 'NONE',  ( -8.000000000000000000, 4.618802153517003184, -4.700000000000000178 ) ) ;
#6063=ADVANCED_FACE ( 'NONE', ( #1079 ), #6866, .T. ) ;
#6079=ORIENTED_EDGE ( 'NONE', *, *, #2924, .T. ) ;
#6082=CARTESIAN_POINT ( 'NONE',  ( 8.000000000000000000, 0.000000000000000000, 2.573333333333333695 ) ) ;
#6085=CIRCLE ( 'NONE', #5451, 8.000000000000000000 ) ;
#6093=DIRECTION ( 'NONE',  ( 0.000000000000000000, -1.000000000000000000, 0.000000000000000000 ) ) ;
#6099=CARTESIAN_POINT ( 'NONE',  ( 8.000000000000000000, 0.000000000000000000, 0.000000000000000000 ) ) ;
#6103=LINE ( 'NONE', #695, #3208 ) ;
#6107=ADVANCED_FACE ( 'NONE', ( #3061, #6570 ), #3614, .F. ) ;
#6111=LINE ( 'NONE', #3044, #5933 ) ;
#6113=FILL_AREA_STYLE ('',( #6666 ) ) ;
#6124=CIRCLE ( 'NONE', #6632, 1.286666666666999914 ) ;
#6148=VERTEX_POINT ( 'NONE', #1202 ) ;
#6154=CARTESIAN_POINT ( 'NONE',  ( 0.000000000000000000, 0.000000000000000000, 3.859999999999999876 ) ) ;
#6174=CIRCLE ( 'NONE', #5413, 5.857142857142856762 ) ;
#6178=STYLED_ITEM('',(#7837),#3145);
#6190=AXIS2_PLACEMENT_3D ( 'NONE', #6585, #7373, #1175 ) ;
#6191=PLANE ( 'NONE',  #7696 ) ;
#6200=VERTEX_POINT ( 'NONE', #725 ) ;
#6204=CARTESIAN_POINT ( 'NONE',  ( -2.644994884459111795, 7.710515798486362371, -0.08224679563971296070 ) ) ;
#6216=DIRECTION ( 'NONE',  ( 1.000000000000000000, 0.000000000000000000, 0.000000000000000000 ) ) ;
#6225=ORIENTED_EDGE ( 'NONE', *, *, #159, .F. ) ;
#6244=PRODUCT_DEFINITION_SHAPE ( 'NONE', 'NONE',  #7394 ) ;
#6259=CARTESIAN_POINT ( 'NONE',  ( 4.000000000000005329, -6.928203230275506108, -4.700000000000000178 ) ) ;
#6261=ORIENTED_EDGE ( 'NONE', *, *, #4278, .F. ) ;
#6262=ORIENTED_EDGE ( 'NONE', *, *, #5047, .F. ) ;
#6265=CIRCLE ( 'NONE', #462, 5.000000000000000888 ) ;
#6267=CARTESIAN_POINT ( 'NONE',  ( -8.000000000000000000, -4.618802153517012954, -4.700000000000000178 ) ) ;
#6268=CARTESIAN_POINT ( 'NONE',  ( -8.000000000000000000, 0.7809653281576030004, 7.623296525288699970E-18 ) ) ;
#6287=ORIENTED_EDGE ( 'NONE', *, *, #1240, .T. ) ;
#6294=DIRECTION ( 'NONE',  ( 1.000000000000000000, 0.000000000000000000, 0.000000000000000000 ) ) ;
#6303=EDGE_CURVE ( 'NONE', #6148, #544, #7340, .T. ) ;
#6312=EDGE_CURVE ( 'NONE', #1789, #6313, #5061, .T. ) ;
#6313=VERTEX_POINT ( 'NONE', #2623 ) ;
#6317=DIRECTION ( 'NONE',  ( -0.000000000000000000, -0.000000000000000000, 1.000000000000000000 ) ) ;
#6324=CARTESIAN_POINT ( 'NONE',  ( -5.857142857142856762, 7.172931252148783106E-16, 2.573333333332999739 ) ) ;
#6330=LINE ( 'NONE', #6955, #4099 ) ;
#6337=ORIENTED_EDGE ( 'NONE', *, *, #6312, .T. ) ;
#6364=CARTESIAN_POINT ( 'NONE',  ( -4.000000000000004441, -6.928203230275506108, -4.700000000000000178 ) ) ;
#6365=EDGE_CURVE ( 'NONE', #544, #6903, #171, .T. ) ;
#6371=DIRECTION ( 'NONE',  ( 1.000000000000000000, 0.000000000000000000, 0.000000000000000000 ) ) ;
#6375=VERTEX_POINT ( 'NONE', #5688 ) ;
#6380=DIRECTION ( 'NONE',  ( 0.000000000000000000, 0.000000000000000000, 1.000000000000000000 ) ) ;
#6382=CARTESIAN_POINT ( 'NONE',  ( 7.347286611336969031, 4.995646404165278831, -0.4969600502617517734 ) ) ;
#6383=CARTESIAN_POINT ( 'NONE',  ( -8.000000000000000000, 0.000000000000000000, 0.000000000000000000 ) ) ;
#6408=CARTESIAN_POINT ( 'NONE',  ( 0.000000000000000000, 0.000000000000000000, 19.04999999999997229 ) ) ;
#6412=DIRECTION ( 'NONE',  ( -0.000000000000000000, -0.000000000000000000, -1.000000000000000000 ) ) ;
#6420=CARTESIAN_POINT ( 'NONE',  ( -4.000000000000004441, 6.928203230275506108, -4.700000000000000178 ) ) ;
#6454=CARTESIAN_POINT ( 'NONE',  ( -3.660532965668821248, 7.124194613927619102, -4.700000000000004619 ) ) ;
#6465=DIRECTION ( 'NONE',  ( 0.000000000000000000, 0.000000000000000000, 1.000000000000000000 ) ) ;
#6488=DIRECTION ( 'NONE',  ( -0.000000000000000000, -0.000000000000000000, 1.000000000000000000 ) ) ;
#6492=VERTEX_POINT ( 'NONE', #359 ) ;
#6496=EDGE_CURVE ( 'NONE', #3054, #2582, #593, .T. ) ;
#6519=CARTESIAN_POINT ( 'NONE',  ( -6.689127551062008514, -5.375634714784628621, -4.382649155111343120 ) ) ;
#6523=DIRECTION ( 'NONE',  ( -0.000000000000000000, -0.000000000000000000, 1.000000000000000000 ) ) ;
#6526=CARTESIAN_POINT ( 'NONE',  ( -8.000000000000001776, -3.867591403079179813, -4.202324684675414979 ) ) ;
#6535=CARTESIAN_POINT ( 'NONE',  ( -7.345652830558760726, 4.996589667937370471, -0.4964154566687939973 ) ) ;
#6538=FACE_OUTER_BOUND ( 'NONE', #1211, .T. ) ;
#6543=ADVANCED_FACE ( 'NONE', ( #6951 ), #3308, .F. ) ;
#6567=CARTESIAN_POINT ( 'NONE',  ( 8.000000000000000000, 1.572549600175618956, -0.06894455525513237815 ) ) ;
#6570=FACE_OUTER_BOUND ( 'NONE', #1725, .T. ) ;
#6573=ORIENTED_EDGE ( 'NONE', *, *, #6496, .T. ) ;
#6585=CARTESIAN_POINT ( 'NONE',  ( 0.000000000000000000, 0.000000000000000000, -4.700000000000000178 ) ) ;
#6586=CARTESIAN_POINT ( 'NONE',  ( -8.000000000000001776, -3.867591403079177592, -0.4976753153245848660 ) ) ;
#6587=( NAMED_UNIT ( * ) PLANE_ANGLE_UNIT ( ) SI_UNIT ( $, .RADIAN. ) );
#6622=CARTESIAN_POINT ( 'NONE',  ( -1.734723475976807094E-15, 9.237604307034017026, -3.985468820183668104 ) ) ;
#6628=FACE_OUTER_BOUND ( 'NONE', #2570, .T. ) ;
#6632=AXIS2_PLACEMENT_3D ( 'NONE', #802, #5731, #326 ) ;
#6640=ORIENTED_EDGE ( 'NONE', *, *, #3269, .F. ) ;
#6646=CARTESIAN_POINT ( 'NONE',  ( 2.503857664561936813E-16, -9.237604307034025908, -4.700000000000000178 ) ) ;
#6666=FILL_AREA_STYLE_COLOUR ( '', #6747 ) ;
#6669=ORIENTED_EDGE ( 'NONE', *, *, #2077, .T. ) ;
#6703=CARTESIAN_POINT ( 'NONE',  ( 5.354491962338131295, -6.146186931204413284, -4.631901280394567166 ) ) ;
#6709=DIRECTION ( 'NONE',  ( 1.000000000000000000, 1.776356839400250465E-15, 0.000000000000000000 ) ) ;
#6723=ORIENTED_EDGE ( 'NONE', *, *, #2501, .T. ) ;
#6733=DIRECTION ( 'NONE',  ( 1.000000000000000000, 0.000000000000000000, 0.000000000000000000 ) ) ;
#6740=EDGE_CURVE ( 'NONE', #6375, #1789, #5942, .T. ) ;
#6742=FACE_OUTER_BOUND ( 'NONE', #1365, .T. ) ;
#6745=CARTESIAN_POINT ( 'NONE',  ( 5.000000000000000888, 0.000000000000000000, -4.699999999999999289 ) ) ;
#6747=COLOUR_RGB ( '',1.000000000000000000, 0.9490196078431372140, 0.9098039215686274384 ) ;
#6761=ORIENTED_EDGE ( 'NONE', *, *, #4327, .T. ) ;
#6766=DIRECTION ( 'NONE',  ( 0.000000000000000000, 0.000000000000000000, 1.000000000000000000 ) ) ;
#6767=CARTESIAN_POINT ( 'NONE',  ( 4.250000000000000000, 0.000000000000000000, -4.700000000000000178 ) ) ;
#6768=ORIENTED_EDGE ( 'NONE', *, *, #4084, .F. ) ;
#6773=VECTOR ( 'NONE', #2706, 1000.000000000000000 ) ;
#6788=AXIS2_PLACEMENT_3D ( 'NONE', #1664, #4062, #7732 ) ;
#6811=FACE_OUTER_BOUND ( 'NONE', #4413, .T. ) ;
#6828=ORIENTED_EDGE ( 'NONE', *, *, #2752, .T. ) ;
#6829=EDGE_CURVE ( 'NONE', #2329, #980, #2741, .T. ) ;
#6857=ORIENTED_EDGE ( 'NONE', *, *, #2685, .T. ) ;
#6860=DIRECTION ( 'NONE',  ( 0.000000000000000000, 0.000000000000000000, 1.000000000000000000 ) ) ;
#6866=CONICAL_SURFACE ( 'NONE', #4217, 8.000000000000000000, 1.047197551196596299 ) ;
#6879=EDGE_CURVE ( 'NONE', #4484, #3551, #6085, .T. ) ;
#6880=DIRECTION ( 'NONE',  ( 0.000000000000000000, 0.000000000000000000, 1.000000000000000000 ) ) ;
#6888=DIRECTION ( 'NONE',  ( -1.000000000000000000, 0.000000000000000000, -0.000000000000000000 ) ) ;
#6890=EDGE_CURVE ( 'NONE', #3121, #4116, #1243, .T. ) ;
#6898=B_SPLINE_CURVE_WITH_KNOTS ( 'NONE', 3,
 ( #1168, #2336, #1090, #1128, #585, #1777 ),
 .UNSPECIFIED., .F., .F.,
 ( 4, 2, 4 ),
 ( 2.380731629581968059E-07, 0.002336973833157553800, 0.004673709593152148775 ),
 .UNSPECIFIED. ) ;
#6900=DIRECTION ( 'NONE',  ( 0.000000000000000000, 0.000000000000000000, -1.000000000000000000 ) ) ;
#6903=VERTEX_POINT ( 'NONE', #5206 ) ;
#6906=AXIS2_PLACEMENT_3D ( 'NONE', #1077, #4036, #5344 ) ;
#6907=CARTESIAN_POINT ( 'NONE',  ( 0.000000000000000000, 0.000000000000000000, -4.700000000000000178 ) ) ;
#6909=CARTESIAN_POINT ( 'NONE',  ( 0.6527133886630217541, -8.860760056385757366, -0.4969600502617634863 ) ) ;
#6911=B_SPLINE_CURVE_WITH_KNOTS ( 'NONE', 3,
 ( #3744, #3078, #1367, #6703, #777, #4844 ),
 .UNSPECIFIED., .F., .F.,
 ( 4, 2, 4 ),
 ( 2.380731629582276432E-07, 0.002336973833157553367, 0.004673709593152147908 ),
 .UNSPECIFIED. ) ;
#6923=CARTESIAN_POINT ( 'NONE',  ( -5.000000000000000888, 0.000000000000000000, -4.674599999999997202 ) ) ;
#6925=DIRECTION ( 'NONE',  ( 0.000000000000000000, 0.000000000000000000, 1.000000000000000000 ) ) ;
#6930=AXIS2_PLACEMENT_3D ( 'NONE', #5704, #6900, #1528 ) ;
#6932=ADVANCED_FACE ( 'NONE', ( #4652 ), #1546, .T. ) ;
#6951=FACE_OUTER_BOUND ( 'NONE', #1289, .T. ) ;
#6955=CARTESIAN_POINT ( 'NONE',  ( 5.857142857142855874, 0.000000000000000000, 9.480888224575629408 ) ) ;
#6967=ORIENTED_EDGE ( 'NONE', *, *, #2259, .T. ) ;
#6971=CARTESIAN_POINT ( 'NONE',  ( 8.000000000000000000, -3.867591403079175372, -0.4976753153245848660 ) ) ;
#6978=ORIENTED_EDGE ( 'NONE', *, *, #4315, .T. ) ;
#6980=ORIENTED_EDGE ( 'NONE', *, *, #4507, .T. ) ;
#6987=ORIENTED_EDGE ( 'NONE', *, *, #5047, .T. ) ;
#6996=CARTESIAN_POINT ( 'NONE',  ( -8.000000000000000000, -4.618802153517013842, -0.7145311798163319628 ) ) ;
#7002=DIRECTION ( 'NONE',  ( -1.000000000000000000, 0.000000000000000000, 0.000000000000000000 ) ) ;
#7006=CARTESIAN_POINT ( 'NONE',  ( -5.354491962338124189, 6.146186931204407067, -4.631901280394571607 ) ) ;
#7013=AXIS2_PLACEMENT_3D ( 'NONE', #7703, #6523, #4628 ) ;
#7018=DIRECTION ( 'NONE',  ( 1.000000000000000000, 0.000000000000000000, 0.000000000000000000 ) ) ;
#7042=DIRECTION ( 'NONE',  ( 1.000000000000000000, 0.000000000000000000, 0.000000000000000000 ) ) ;
#7048=CARTESIAN_POINT ( 'NONE',  ( 4.000000000000004441, 6.928203230275507885, 0.000000000000000000 ) ) ;
#7072=CARTESIAN_POINT ( 'NONE',  ( -4.339467034331195627, -6.732211846623401108, -1.075167154381460273E-15 ) ) ;
#7077=B_SPLINE_CURVE_WITH_KNOTS ( 'NONE', 3,
 ( #5891, #2320, #6567, #713, #7740, #2359 ),
 .UNSPECIFIED., .F., .F.,
 ( 4, 2, 4 ),
 ( 0.01291313371729457642, 0.01525081363757309350, 0.01758849355785160884 ),
 .UNSPECIFIED. ) ;
#7079=ORIENTED_EDGE ( 'NONE', *, *, #2358, .T. ) ;
#7094=UNCERTAINTY_MEASURE_WITH_UNIT (LENGTH_MEASURE( 1.000000000000000082E-05 ), #2964, 'distance_accuracy_value', 'NONE');
#7108=ORIENTED_EDGE ( 'NONE', *, *, #4084, .T. ) ;
#7132=CARTESIAN_POINT ( 'NONE',  ( 0.000000000000000000, 0.000000000000000000, -4.700000000000000178 ) ) ;
#7139=CARTESIAN_POINT ( 'NONE',  ( 0.000000000000000000, 0.000000000000000000, 2.573333333332999739 ) ) ;
#7145=FACE_OUTER_BOUND ( 'NONE', #4691, .T. ) ;
#7164=CARTESIAN_POINT ( 'NONE',  ( -4.000000000000004441, 6.928203230275506108, -4.700000000000000178 ) ) ;
#7173=ORIENTED_EDGE ( 'NONE', *, *, #5323, .T. ) ;
#7177=ORIENTED_EDGE ( 'NONE', *, *, #426, .F. ) ;
#7182=EDGE_CURVE ( 'NONE', #2329, #1610, #5457, .T. ) ;
#7190=AXIS2_PLACEMENT_3D ( 'NONE', #514, #3556, #5372 ) ;
#7199=DIRECTION ( 'NONE',  ( -0.000000000000000000, -0.000000000000000000, -1.000000000000000000 ) ) ;
#7210=ORIENTED_EDGE ( 'NONE', *, *, #94, .F. ) ;
#7214=ORIENTED_EDGE ( 'NONE', *, *, #6879, .T. ) ;
#7217=EDGE_CURVE ( 'NONE', #7619, #3392, #787, .T. ) ;
#7250=CARTESIAN_POINT ( 'NONE',  ( 8.000000000000000000, 0.000000000000000000, 9.480888224575629408 ) ) ;
#7258=SHAPE_REPRESENTATION_RELATIONSHIP ( 'NONE' , 'NONE' ,  #1433, #7262 ) ;
#7262=ADVANCED_BREP_SHAPE_REPRESENTATION ( '', ( #3145, #7485 ), #309 ) ;
#7266=CARTESIAN_POINT ( 'NONE',  ( -0.6543471694412565931, -8.859816792613647962, -0.4964154566687977721 ) ) ;
#7301=ORIENTED_EDGE ( 'NONE', *, *, #2684, .T. ) ;
#7316=ADVANCED_FACE ( 'NONE', ( #7424 ), #1550, .F. ) ;
#7327=SHAPE_DEFINITION_REPRESENTATION ( #6244, #1433 ) ;
#7334=ORIENTED_EDGE ( 'NONE', *, *, #94, .T. ) ;
#7336=CARTESIAN_POINT ( 'NONE',  ( 5.000000000000000888, 6.123233995736767268E-16, -4.674599999999997202 ) ) ;
#7340=CIRCLE ( 'NONE', #4812, 4.250000000000000000 ) ;
#7344=DIRECTION ( 'NONE',  ( 1.000000000000000000, 0.000000000000000000, 0.000000000000000000 ) ) ;
#7345=CARTESIAN_POINT ( 'NONE',  ( 3.319543390096037605, -7.321065037175434220, -0.01688885742777183549 ) ) ;
#7350=AXIS2_PLACEMENT_3D ( 'NONE', #5382, #6380, #1714 ) ;
#7352=CARTESIAN_POINT ( 'NONE',  ( -8.000000000000000000, 4.618802153517003184, -4.700000000000000178 ) ) ;
#7367=ORIENTED_EDGE ( 'NONE', *, *, #81, .T. ) ;
#7372=B_SPLINE_CURVE_WITH_KNOTS ( 'NONE', 3,
 ( #3052, #7266, #1865, #4262, #4894, #3675 ),
 .UNSPECIFIED., .F., .F.,
 ( 4, 2, 4 ),
 ( 2.380731629811925857E-07, 0.002336973833157575484, 0.004673709593152171327 ),
 .UNSPECIFIED. ) ;
#7373=DIRECTION ( 'NONE',  ( -0.000000000000000000, -0.000000000000000000, 1.000000000000000000 ) ) ;
#7375=( GEOMETRIC_REPRESENTATION_CONTEXT ( 3 ) GLOBAL_UNCERTAINTY_ASSIGNED_CONTEXT ( ( #7094 ) ) GLOBAL_UNIT_ASSIGNED_CONTEXT ( ( #2964, #6587, #112 ) ) REPRESENTATION_CONTEXT ( 'NONE', 'WORKASPACE' ) );
#7381=CARTESIAN_POINT ( 'NONE',  ( 1.310872448937991486, -8.480771745766411129, -0.3173508448886628863 ) ) ;
#7393=AXIS2_PLACEMENT_3D ( 'NONE', #4590, #3962, #6888 ) ;
#7394=PRODUCT_DEFINITION ( 'UNKNOWN', '', #5957, #2986 ) ;
#7403=ORIENTED_EDGE ( 'NONE', *, *, #122, .F. ) ;
#7414=AXIS2_PLACEMENT_3D ( 'NONE', #5236, #5274, #541 ) ;
#7416=AXIS2_PLACEMENT_3D ( 'NONE', #2742, #6412, #6371 ) ;
#7422=ADVANCED_FACE ( 'NONE', ( #5019 ), #4232, .T. ) ;
#7424=FACE_OUTER_BOUND ( 'NONE', #4856, .T. ) ;
#7428=EDGE_LOOP ( 'NONE', ( #3055, #2118, #1493, #5910 ) ) ;
#7462=CARTESIAN_POINT ( 'NONE',  ( 0.000000000000000000, 0.000000000000000000, 2.573333333332999739 ) ) ;
#7474=VECTOR ( 'NONE', #3080, 1000.000000000000000 ) ;
#7475=ORIENTED_EDGE ( 'NONE', *, *, #1971, .F. ) ;
#7485=AXIS2_PLACEMENT_3D ( 'NONE', #1301, #3758, #5977 ) ;
#7525=B_SPLINE_CURVE_WITH_KNOTS ( 'NONE', 3,
 ( #7164, #6454, #5985, #1045, #1729, #3456, #5865, #2910 ),
 .UNSPECIFIED., .F., .F.,
 ( 4, 2, 2, 4 ),
 ( 0.004673709593152153112, 0.005837709341827643401, 0.007001709090503134558, 0.009329708587854111668 ),
 .UNSPECIFIED. ) ;
#7533=CARTESIAN_POINT ( 'NONE',  ( -3.660532965668821248, 7.124194613927619102, 4.997070872326744850E-15 ) ) ;
#7537=VERTEX_POINT ( 'NONE', #6324 ) ;
#7540=DIRECTION ( 'NONE',  ( -0.000000000000000000, -0.000000000000000000, 1.000000000000000000 ) ) ;
#7547=LINE ( 'NONE', #880, #95 ) ;
#7573=CARTESIAN_POINT ( 'NONE',  ( 4.000000000000004441, 6.928203230275507885, -4.700000000000000178 ) ) ;
#7611=ORIENTED_EDGE ( 'NONE', *, *, #6303, .T. ) ;
#7619=VERTEX_POINT ( 'NONE', #6923 ) ;
#7621=CARTESIAN_POINT ( 'NONE',  ( -5.690023276062397883, -5.952467836904158816, -0.1306530452038143220 ) ) ;
#7637=DIRECTION ( 'NONE',  ( 1.000000000000000000, 0.000000000000000000, 0.000000000000000000 ) ) ;
#7640=CIRCLE ( 'NONE', #2242, 8.000000000000000000 ) ;
#7646=DIRECTION ( 'NONE',  ( 0.000000000000000000, 0.000000000000000000, 1.000000000000000000 ) ) ;
#7649=ORIENTED_EDGE ( 'NONE', *, *, #7217, .F. ) ;
#7670=ORIENTED_EDGE ( 'NONE', *, *, #3357, .T. ) ;
#7674=DIRECTION ( 'NONE',  ( 1.000000000000000000, 0.000000000000000000, 0.000000000000000000 ) ) ;
#7678=AXIS2_PLACEMENT_3D ( 'NONE', #5476, #3118, #111 ) ;
#7689=VERTEX_POINT ( 'NONE', #3332 ) ;
#7696=AXIS2_PLACEMENT_3D ( 'NONE', #6267, #225, #1488 ) ;
#7699=ORIENTED_EDGE ( 'NONE', *, *, #1971, .T. ) ;
#7703=CARTESIAN_POINT ( 'NONE',  ( 0.000000000000000000, 0.000000000000000000, 9.480888224575629408 ) ) ;
#7707=CYLINDRICAL_SURFACE ( 'NONE', #1193, 8.000000000000000000 ) ;
#7717=CARTESIAN_POINT ( 'NONE',  ( -8.000000000000000000, 0.000000000000000000, 0.000000000000000000 ) ) ;
#7719=EDGE_LOOP ( 'NONE', ( #7173, #4373, #6761, #5602, #493, #3156 ) ) ;
#7722=CARTESIAN_POINT ( 'NONE',  ( -8.000000000000000000, 1.572549600175617401, -4.631055444744868410 ) ) ;
#7726=VECTOR ( 'NONE', #7646, 1000.000000000000000 ) ;
#7732=DIRECTION ( 'NONE',  ( 1.000000000000000000, 0.000000000000000000, 0.000000000000000000 ) ) ;
#7740=CARTESIAN_POINT ( 'NONE',  ( 8.000000000000000000, 3.871967595402126872, -0.4989386132324573064 ) ) ;
#7749=CARTESIAN_POINT ( 'NONE',  ( -4.681481898397001018, 6.534749472788146996, -4.700000000000005507 ) ) ;
#7762=CARTESIAN_POINT ( 'NONE',  ( -8.000000000000000000, 0.7809653281576043327, -4.700000000000000178 ) ) ;
#7831=COLOUR_RGB('Black',0.12,0.14,0.17);
#7832=FILL_AREA_STYLE_COLOUR('',#7831);
#7833=FILL_AREA_STYLE('',(#7832));
#7834=SURFACE_STYLE_FILL_AREA(#7833);
#7835=SURFACE_SIDE_STYLE('',(#7834));
#7836=SURFACE_STYLE_USAGE(.BOTH.,#7835);
#7837=PRESENTATION_STYLE_ASSIGNMENT((#7836));
ENDSEC;
END-ISO-10303-21;
